ISO-10303-21;
HEADER;
FILE_DESCRIPTION (('STEP AP214'),
    '1' );
FILE_NAME ('Part8.step',
    '2026-11-01T05:08:46',
    ( '' ),
    ( '' ),
    'SwSTEP 2.0',
    'SolidWorks 2024',
    '' );
FILE_SCHEMA (( 'AUTOMOTIVE_DESIGN' ));
ENDSEC;

DATA;
#9=PLANE ( 'NONE',  #8732 ) ;
#19=EDGE_LOOP ( 'NONE', ( #9560, #531, #12122, #8453 ) ) ;
#22=EDGE_CURVE ( 'NONE', #12299, #3010, #16896, .T. ) ;
#35=ORIENTED_EDGE ( 'NONE', *, *, #6969, .T. ) ;
#49=VERTEX_POINT ( 'NONE', #336 ) ;
#56=VECTOR ( 'NONE', #6748, 1000.000000000000000 ) ;
#88=CARTESIAN_POINT ( 'NONE',  ( 394.0000000000001137, 339.1725919290087745, -9.945665743359786148 ) ) ;
#94=VECTOR ( 'NONE', #8988, 1000.000000000000000 ) ;
#101=LINE ( 'NONE', #5412, #10344 ) ;
#106=ORIENTED_EDGE ( 'NONE', *, *, #6625, .F. ) ;
#111=CIRCLE ( 'NONE', #1754, 6.473199999999998511 ) ;
#129=DIRECTION ( 'NONE',  ( 0.000000000000000000, -1.000000000000000000, -1.321694076934710402E-16 ) ) ;
#159=DIRECTION ( 'NONE',  ( -1.000000000000000000, -0.000000000000000000, -0.000000000000000000 ) ) ;
#163=CARTESIAN_POINT ( 'NONE',  ( 394.0000000000001137, 240.0523724647196389, -110.6822657433598067 ) ) ;
#187=ORIENTED_EDGE ( 'NONE', *, *, #2247, .T. ) ;
#213=LINE ( 'NONE', #14888, #5281 ) ;
#250=ORIENTED_EDGE ( 'NONE', *, *, #16480, .F. ) ;
#284=ORIENTED_EDGE ( 'NONE', *, *, #16141, .F. ) ;
#285=ADVANCED_FACE ( 'NONE', ( #926 ), #12433, .F. ) ;
#312=CARTESIAN_POINT ( 'NONE',  ( 394.0000000000001137, 339.1725919290084335, -104.9456657433597968 ) ) ;
#333=ORIENTED_EDGE ( 'NONE', *, *, #8889, .F. ) ;
#334=LINE ( 'NONE', #2990, #5479 ) ;
#336=CARTESIAN_POINT ( 'NONE',  ( 0.000000000000000000, 234.3157724647196289, -17.15546574335979813 ) ) ;
#337=AXIS2_PLACEMENT_3D ( 'NONE', #6271, #15489, #13602 ) ;
#357=DIRECTION ( 'NONE',  ( 1.000000000000000000, 0.000000000000000000, -0.000000000000000000 ) ) ;
#406=DIRECTION ( 'NONE',  ( 1.000000000000000000, -0.000000000000000000, -0.000000000000000000 ) ) ;
#433=LINE ( 'NONE', #5661, #11650 ) ;
#445=DIRECTION ( 'NONE',  ( 0.000000000000000000, 0.9271838545667883125, 0.3746065934159094613 ) ) ;
#446=FACE_OUTER_BOUND ( 'NONE', #19, .T. ) ;
#458=AXIS2_PLACEMENT_3D ( 'NONE', #2840, #8249, #10918 ) ;
#494=DIRECTION ( 'NONE',  ( 0.000000000000000000, 0.000000000000000000, -1.000000000000000000 ) ) ;
#504=EDGE_CURVE ( 'NONE', #11776, #6598, #7167, .T. ) ;
#531=ORIENTED_EDGE ( 'NONE', *, *, #13661, .F. ) ;
#543=DIRECTION ( 'NONE',  ( 0.000000000000000000, 0.3746065934159052424, -0.9271838545667901998 ) ) ;
#583=VERTEX_POINT ( 'NONE', #11907 ) ;
#587=EDGE_CURVE ( 'NONE', #1572, #3874, #1682, .T. ) ;
#633=ORIENTED_EDGE ( 'NONE', *, *, #4265, .T. ) ;
#642=VECTOR ( 'NONE', #7917, 1000.000000000000000 ) ;
#652=LINE ( 'NONE', #5966, #6353 ) ;
#670=MECHANICAL_DESIGN_GEOMETRIC_PRESENTATION_REPRESENTATION('',(#13291),#13993);
#676=AXIS2_PLACEMENT_3D ( 'NONE', #3456, #5688, #10932 ) ;
#678=DIRECTION ( 'NONE',  ( -1.000000000000000000, -0.000000000000000000, -0.000000000000000000 ) ) ;
#696=EDGE_CURVE ( 'NONE', #1365, #12299, #5834, .T. ) ;
#700=EDGE_CURVE ( 'NONE', #3010, #49, #652, .T. ) ;
#727=SHAPE_REPRESENTATION_RELATIONSHIP ( 'NONE' , 'NONE' ,  #12962, #7706 ) ;
#728=VECTOR ( 'NONE', #16402, 1000.000000000000000 ) ;
#755=FACE_OUTER_BOUND ( 'NONE', #10542, .T. ) ;
#770=EDGE_CURVE ( 'NONE', #8036, #5137, #1240, .T. ) ;
#774=ORIENTED_EDGE ( 'NONE', *, *, #13513, .F. ) ;
#791=ADVANCED_FACE ( 'NONE', ( #16939 ), #2512, .T. ) ;
#808=EDGE_CURVE ( 'NONE', #12512, #9815, #9142, .T. ) ;
#813=CARTESIAN_POINT ( 'NONE',  ( 394.0000000000001137, 341.5974953295075807, -105.4170192159777031 ) ) ;
#824=DIRECTION ( 'NONE',  ( 0.000000000000000000, -1.000000000000000000, -1.321694076934710402E-16 ) ) ;
#831=CARTESIAN_POINT ( 'NONE',  ( 0.000000000000000000, 339.1725919290087745, -16.41886574335978821 ) ) ;
#834=CARTESIAN_POINT ( 'NONE',  ( 0.000000000000000000, 339.1725919290087745, -10.68226574335978718 ) ) ;
#863=DIRECTION ( 'NONE',  ( 0.000000000000000000, -0.3746065934159095168, 0.9271838545667885345 ) ) ;
#884=VERTEX_POINT ( 'NONE', #2349 ) ;
#890=EDGE_CURVE ( 'NONE', #6948, #14037, #11627, .T. ) ;
#891=FACE_OUTER_BOUND ( 'NONE', #5859, .T. ) ;
#914=DIRECTION ( 'NONE',  ( 1.000000000000000000, 0.000000000000000000, -0.000000000000000000 ) ) ;
#918=ADVANCED_FACE ( 'NONE', ( #13526 ), #5515, .T. ) ;
#926=FACE_OUTER_BOUND ( 'NONE', #7504, .T. ) ;
#973=ORIENTED_EDGE ( 'NONE', *, *, #6528, .F. ) ;
#1001=CARTESIAN_POINT ( 'NONE',  ( 394.0000000000001137, 339.1725919290084335, -111.4188657433597456 ) ) ;
#1010=LINE ( 'NONE', #3831, #8134 ) ;
#1020=ADVANCED_FACE ( 'NONE', ( #13178 ), #1403, .T. ) ;
#1025=ORIENTED_EDGE ( 'NONE', *, *, #8889, .T. ) ;
#1033=ORIENTED_EDGE ( 'NONE', *, *, #15874, .T. ) ;
#1057=CARTESIAN_POINT ( 'NONE',  ( 0.000000000000000000, 234.3157724647196289, -17.15546574335979813 ) ) ;
#1066=DIRECTION ( 'NONE',  ( 0.000000000000000000, 1.000000000000000000, 1.321694076934710402E-16 ) ) ;
#1077=LINE ( 'NONE', #1250, #94 ) ;
#1082=VERTEX_POINT ( 'NONE', #3527 ) ;
#1084=FACE_OUTER_BOUND ( 'NONE', #9002, .T. ) ;
#1089=CARTESIAN_POINT ( 'NONE',  ( 394.0000000000001137, 240.7889724647196488, -16.41886574335980242 ) ) ;
#1091=PLANE ( 'NONE',  #3181 ) ;
#1096=ADVANCED_FACE ( 'NONE', ( #3607 ), #16731, .F. ) ;
#1133=DIRECTION ( 'NONE',  ( -1.000000000000000000, -0.000000000000000000, -0.000000000000000000 ) ) ;
#1189=CARTESIAN_POINT ( 'NONE',  ( 394.0000000000001137, 451.4647406485092915, -149.8062676851188257 ) ) ;
#1200=EDGE_CURVE ( 'NONE', #8036, #5519, #15702, .T. ) ;
#1209=VECTOR ( 'NONE', #1133, 1000.000000000000000 ) ;
#1233=VERTEX_POINT ( 'NONE', #11671 ) ;
#1240=LINE ( 'NONE', #2612, #7194 ) ;
#1250=CARTESIAN_POINT ( 'NONE',  ( 394.0000000000001137, 339.3157724647196005, -104.9456657433597968 ) ) ;
#1251=ORIENTED_EDGE ( 'NONE', *, *, #13170, .T. ) ;
#1271=ORIENTED_EDGE ( 'NONE', *, *, #7467, .F. ) ;
#1273=LINE ( 'NONE', #10299, #16887 ) ;
#1288=EDGE_LOOP ( 'NONE', ( #9754, #15029, #5415, #13991 ) ) ;
#1337=CARTESIAN_POINT ( 'NONE',  ( 0.000000000000000000, 234.3157724647196289, -17.15546574335979813 ) ) ;
#1345=ORIENTED_EDGE ( 'NONE', *, *, #16480, .T. ) ;
#1352=ORIENTED_EDGE ( 'NONE', *, *, #8341, .F. ) ;
#1365=VERTEX_POINT ( 'NONE', #1623 ) ;
#1403=PLANE ( 'NONE',  #13541 ) ;
#1442=DIRECTION ( 'NONE',  ( -0.000000000000000000, -0.000000000000000000, 1.000000000000000000 ) ) ;
#1448=DIRECTION ( 'NONE',  ( -1.000000000000000000, -0.000000000000000000, -0.000000000000000000 ) ) ;
#1474=ORIENTED_EDGE ( 'NONE', *, *, #16537, .T. ) ;
#1485=DIRECTION ( 'NONE',  ( 0.000000000000000000, 0.000000000000000000, 1.000000000000000000 ) ) ;
#1488=AXIS2_PLACEMENT_3D ( 'NONE', #3280, #8693, #15217 ) ;
#1529=CARTESIAN_POINT ( 'NONE',  ( 394.0000000000001137, 234.3157724647196289, -110.6822657433598067 ) ) ;
#1530=ORIENTED_EDGE ( 'NONE', *, *, #2037, .F. ) ;
#1547=PLANE ( 'NONE',  #13313 ) ;
#1572=VERTEX_POINT ( 'NONE', #8201 ) ;
#1578=LINE ( 'NONE', #8267, #7825 ) ;
#1597=CARTESIAN_POINT ( 'NONE',  ( 394.0000000000001137, 240.7889724647196488, -10.68226574335980139 ) ) ;
#1608=CARTESIAN_POINT ( 'NONE',  ( 0.000000000000000000, 339.3157724647196005, -10.68226574335978718 ) ) ;
#1611=DIRECTION ( 'NONE',  ( 0.000000000000000000, 0.000000000000000000, 1.000000000000000000 ) ) ;
#1623=CARTESIAN_POINT ( 'NONE',  ( 394.0000000000001137, 240.7889724647196488, -110.6822657433598067 ) ) ;
#1644=VERTEX_POINT ( 'NONE', #312 ) ;
#1660=DIRECTION ( 'NONE',  ( 0.000000000000000000, 0.3746065934159049093, 0.9271838545667903109 ) ) ;
#1682=LINE ( 'NONE', #14664, #11577 ) ;
#1715=LINE ( 'NONE', #13412, #8835 ) ;
#1752=ADVANCED_FACE ( 'NONE', ( #2255 ), #10166, .T. ) ;
#1754=AXIS2_PLACEMENT_3D ( 'NONE', #12159, #10609, #15844 ) ;
#1779=DIRECTION ( 'NONE',  ( 0.000000000000000000, -6.028905917052134721E-13, 1.000000000000000000 ) ) ;
#1783=ORIENTED_EDGE ( 'NONE', *, *, #5969, .T. ) ;
#1801=ORIENTED_EDGE ( 'NONE', *, *, #2153, .F. ) ;
#1822=ORIENTED_EDGE ( 'NONE', *, *, #16704, .F. ) ;
#1825=EDGE_LOOP ( 'NONE', ( #1352, #16758, #14728, #15352 ) ) ;
#1856=ADVANCED_FACE ( 'NONE', ( #9208 ), #9, .T. ) ;
#1879=VERTEX_POINT ( 'NONE', #15718 ) ;
#1893=FILL_AREA_STYLE_COLOUR ( '', #14103 ) ;
#1905=DIRECTION ( 'NONE',  ( -1.000000000000000000, -0.000000000000000000, -0.000000000000000000 ) ) ;
#1933=VECTOR ( 'NONE', #15848, 1000.000000000000000 ) ;
#1960=EDGE_CURVE ( 'NONE', #14037, #7396, #11760, .T. ) ;
#1988=CARTESIAN_POINT ( 'NONE',  ( 0.000000000000000000, 240.7889724647196488, -10.68226574335980139 ) ) ;
#1992=CARTESIAN_POINT ( 'NONE',  ( 394.0000000000001137, 339.1725919290087745, -9.945665743359786148 ) ) ;
#2019=ORIENTED_EDGE ( 'NONE', *, *, #11303, .T. ) ;
#2029=DIRECTION ( 'NONE',  ( 0.000000000000000000, 0.000000000000000000, -1.000000000000000000 ) ) ;
#2037=EDGE_CURVE ( 'NONE', #7396, #884, #9721, .T. ) ;
#2075=VERTEX_POINT ( 'NONE', #15288 ) ;
#2147=APPLICATION_CONTEXT ( 'automotive_design' ) ;
#2152=ORIENTED_EDGE ( 'NONE', *, *, #890, .T. ) ;
#2153=EDGE_CURVE ( 'NONE', #14413, #13380, #15617, .T. ) ;
#2159=CARTESIAN_POINT ( 'NONE',  ( 394.0000000000001137, 339.3157724647196005, -10.68226574335978718 ) ) ;
#2160=EDGE_LOOP ( 'NONE', ( #3106, #13738, #4544, #14107 ) ) ;
#2173=CARTESIAN_POINT ( 'NONE',  ( 0.000000000000000000, 339.3157724647196005, -104.9456657433597968 ) ) ;
#2247=EDGE_CURVE ( 'NONE', #16075, #1365, #13374, .T. ) ;
#2255=FACE_OUTER_BOUND ( 'NONE', #2494, .T. ) ;
#2262=ADVANCED_FACE ( 'NONE', ( #7788 ), #5633, .F. ) ;
#2278=DIRECTION ( 'NONE',  ( 0.000000000000000000, -6.028905917052134721E-13, 1.000000000000000000 ) ) ;
#2308=CARTESIAN_POINT ( 'NONE',  ( 394.0000000000001137, 341.4647406485092915, -16.00114864346762644 ) ) ;
#2338=AXIS2_PLACEMENT_3D ( 'NONE', #10946, #8276, #16097 ) ;
#2339=PLANE ( 'NONE',  #337 ) ;
#2343=DIRECTION ( 'NONE',  ( 1.000000000000000000, 0.000000000000000000, -0.000000000000000000 ) ) ;
#2345=CARTESIAN_POINT ( 'NONE',  ( 394.0000000000001137, 451.4647406485094621, 28.44173619839933309 ) ) ;
#2349=CARTESIAN_POINT ( 'NONE',  ( 0.000000000000000000, 451.4647406485094621, 28.44173619839933309 ) ) ;
#2396=DIRECTION ( 'NONE',  ( 0.000000000000000000, -0.3746065934159049648, -0.9271838545667903109 ) ) ;
#2401=ORIENTED_EDGE ( 'NONE', *, *, #2476, .F. ) ;
#2414=ORIENTED_EDGE ( 'NONE', *, *, #16539, .T. ) ;
#2429=CARTESIAN_POINT ( 'NONE',  ( 0.000000000000000000, 451.4647406485092915, -149.8062676851188257 ) ) ;
#2430=CARTESIAN_POINT ( 'NONE',  ( 0.000000000000000000, 339.3157724647196005, -16.41886574335978821 ) ) ;
#2433=ORIENTED_EDGE ( 'NONE', *, *, #5335, .F. ) ;
#2435=DIRECTION ( 'NONE',  ( 0.000000000000000000, 0.000000000000000000, 1.000000000000000000 ) ) ;
#2448=DIRECTION ( 'NONE',  ( -1.000000000000000000, -0.000000000000000000, -0.000000000000000000 ) ) ;
#2476=EDGE_CURVE ( 'NONE', #12820, #14037, #6620, .T. ) ;
#2494=EDGE_LOOP ( 'NONE', ( #16571, #5730, #15677, #9076 ) ) ;
#2496=EDGE_LOOP ( 'NONE', ( #2651, #12373, #14289, #8279 ) ) ;
#2512=PLANE ( 'NONE',  #8316 ) ;
#2524=AXIS2_PLACEMENT_3D ( 'NONE', #6774, #9624, #15878 ) ;
#2555=EDGE_CURVE ( 'NONE', #5137, #1233, #14629, .T. ) ;
#2585=DIRECTION ( 'NONE',  ( 0.000000000000000000, 0.000000000000000000, 1.000000000000000000 ) ) ;
#2606=EDGE_CURVE ( 'NONE', #7927, #9826, #14377, .T. ) ;
#2612=CARTESIAN_POINT ( 'NONE',  ( 0.000000000000000000, 451.4647406485092915, -149.8062676851188257 ) ) ;
#2625=DIRECTION ( 'NONE',  ( 0.000000000000000000, 0.000000000000000000, 1.000000000000000000 ) ) ;
#2651=ORIENTED_EDGE ( 'NONE', *, *, #8048, .F. ) ;
#2668=CARTESIAN_POINT ( 'NONE',  ( 394.0000000000001137, 451.4647406485092915, -149.8062676851188257 ) ) ;
#2677=EDGE_CURVE ( 'NONE', #12299, #1082, #213, .T. ) ;
#2689=DIRECTION ( 'NONE',  ( 0.000000000000000000, 0.000000000000000000, -1.000000000000000000 ) ) ;
#2709=DIRECTION ( 'NONE',  ( 0.000000000000000000, 1.000000000000000000, 0.000000000000000000 ) ) ;
#2729=CARTESIAN_POINT ( 'NONE',  ( 394.0000000000001137, 339.1725919290087745, -10.68226574335978718 ) ) ;
#2764=FACE_OUTER_BOUND ( 'NONE', #11390, .T. ) ;
#2786=CARTESIAN_POINT ( 'NONE',  ( 394.0000000000001137, 339.4485271457185718, -110.7359021160857537 ) ) ;
#2797=VECTOR ( 'NONE', #6916, 1000.000000000000000 ) ;
#2802=ORIENTED_EDGE ( 'NONE', *, *, #5840, .T. ) ;
#2835=DIRECTION ( 'NONE',  ( 0.000000000000000000, 1.000000000000000000, 1.321694076934710402E-16 ) ) ;
#2840=CARTESIAN_POINT ( 'NONE',  ( 394.0000000000001137, 449.3157724647197142, 33.76061909850716347 ) ) ;
#2841=ORIENTED_EDGE ( 'NONE', *, *, #700, .T. ) ;
#2850=AXIS2_PLACEMENT_3D ( 'NONE', #14194, #11695, #6434 ) ;
#2895=EDGE_CURVE ( 'NONE', #12820, #14413, #6670, .T. ) ;
#2901=LINE ( 'NONE', #12423, #9353 ) ;
#2929=EDGE_LOOP ( 'NONE', ( #6123, #1251, #3871, #3791 ) ) ;
#2931=CARTESIAN_POINT ( 'NONE',  ( 394.0000000000001137, 234.3157724647196289, -104.2090657433598011 ) ) ;
#2933=LINE ( 'NONE', #5488, #14159 ) ;
#2952=DIRECTION ( 'NONE',  ( 0.000000000000000000, 1.000000000000000000, 0.000000000000000000 ) ) ;
#2962=ORIENTED_EDGE ( 'NONE', *, *, #13661, .T. ) ;
#2990=CARTESIAN_POINT ( 'NONE',  ( 394.0000000000001137, 449.3157724647197142, 33.76061909850716347 ) ) ;
#3007=FACE_OUTER_BOUND ( 'NONE', #16160, .T. ) ;
#3010=VERTEX_POINT ( 'NONE', #10920 ) ;
#3039=EDGE_LOOP ( 'NONE', ( #2841, #1474, #10325, #16301 ) ) ;
#3041=DIRECTION ( 'NONE',  ( -1.000000000000000000, 0.000000000000000000, 0.000000000000000000 ) ) ;
#3044=CARTESIAN_POINT ( 'NONE',  ( 0.000000000000000000, 449.3157724647196005, -155.1251505852266632 ) ) ;
#3056=ADVANCED_FACE ( 'NONE', ( #7899 ), #15813, .F. ) ;
#3057=DIRECTION ( 'NONE',  ( 0.000000000000000000, 0.000000000000000000, 1.000000000000000000 ) ) ;
#3078=DIRECTION ( 'NONE',  ( 0.000000000000000000, 0.3746065934159141242, -0.9271838545667866471 ) ) ;
#3102=CARTESIAN_POINT ( 'NONE',  ( 394.0000000000001137, 339.1725919290084335, -110.6822657433597925 ) ) ;
#3106=ORIENTED_EDGE ( 'NONE', *, *, #587, .F. ) ;
#3158=VECTOR ( 'NONE', #2835, 1000.000000000000000 ) ;
#3164=MANIFOLD_SOLID_BREP ( 'Base-Flange1', #9370 ) ;
#3181=AXIS2_PLACEMENT_3D ( 'NONE', #14315, #6308, #10117 ) ;
#3241=EDGE_LOOP ( 'NONE', ( #9996, #2414, #973, #8676 ) ) ;
#3248=ORIENTED_EDGE ( 'NONE', *, *, #10358, .F. ) ;
#3273=PRESENTATION_STYLE_ASSIGNMENT (( #12619 ) ) ;
#3278=AXIS2_PLACEMENT_3D ( 'NONE', #3394, #15150, #3057 ) ;
#3280=CARTESIAN_POINT ( 'NONE',  ( 0.000000000000000000, 0.000000000000000000, 0.000000000000000000 ) ) ;
#3369=CARTESIAN_POINT ( 'NONE',  ( 394.0000000000001137, 339.4485271457189128, -10.62862937063367852 ) ) ;
#3394=CARTESIAN_POINT ( 'NONE',  ( 0.000000000000000000, 240.0523724647196389, -104.2090657433598011 ) ) ;
#3399=AXIS2_PLACEMENT_3D ( 'NONE', #8860, #1905, #14013 ) ;
#3443=SURFACE_STYLE_FILL_AREA ( #9808 ) ;
#3456=CARTESIAN_POINT ( 'NONE',  ( 0.000000000000000000, 339.1725919290087745, -9.945665743359786148 ) ) ;
#3462=VERTEX_POINT ( 'NONE', #8491 ) ;
#3472=DIRECTION ( 'NONE',  ( 0.000000000000000000, 0.000000000000000000, 1.000000000000000000 ) ) ;
#3501=DIRECTION ( 'NONE',  ( 0.000000000000000000, 0.000000000000000000, -1.000000000000000000 ) ) ;
#3527=CARTESIAN_POINT ( 'NONE',  ( 394.0000000000001137, 240.0523724647196389, -104.2090657433598011 ) ) ;
#3602=LINE ( 'NONE', #12539, #728 ) ;
#3607=FACE_OUTER_BOUND ( 'NONE', #13615, .T. ) ;
#3640=FACE_OUTER_BOUND ( 'NONE', #7372, .T. ) ;
#3649=EDGE_LOOP ( 'NONE', ( #333, #8327, #4035, #5418 ) ) ;
#3652=ORIENTED_EDGE ( 'NONE', *, *, #8341, .T. ) ;
#3664=CARTESIAN_POINT ( 'NONE',  ( 0.000000000000000000, 240.0523724647196389, -17.15546574335979813 ) ) ;
#3668=DIRECTION ( 'NONE',  ( 1.000000000000000000, -0.000000000000000000, -0.000000000000000000 ) ) ;
#3682=DIRECTION ( 'NONE',  ( -1.000000000000000000, -0.000000000000000000, -0.000000000000000000 ) ) ;
#3750=DIRECTION ( 'NONE',  ( -1.000000000000000000, -0.000000000000000000, -0.000000000000000000 ) ) ;
#3788=LINE ( 'NONE', #9027, #3158 ) ;
#3791=ORIENTED_EDGE ( 'NONE', *, *, #10955, .T. ) ;
#3831=CARTESIAN_POINT ( 'NONE',  ( 394.0000000000001137, 234.3157724647196289, -17.15546574335979813 ) ) ;
#3834=EDGE_CURVE ( 'NONE', #7927, #8784, #8058, .T. ) ;
#3846=CARTESIAN_POINT ( 'NONE',  ( 0.000000000000000000, 339.4485271457185718, -110.7359021160857537 ) ) ;
#3850=FACE_OUTER_BOUND ( 'NONE', #3852, .T. ) ;
#3852=EDGE_LOOP ( 'NONE', ( #6001, #10937, #9903, #3866 ) ) ;
#3866=ORIENTED_EDGE ( 'NONE', *, *, #2606, .T. ) ;
#3871=ORIENTED_EDGE ( 'NONE', *, *, #15156, .T. ) ;
#3874=VERTEX_POINT ( 'NONE', #5718 ) ;
#3876=EDGE_CURVE ( 'NONE', #1572, #1879, #16195, .T. ) ;
#3887=CARTESIAN_POINT ( 'NONE',  ( 394.0000000000001137, 339.1725919290084335, -104.9456657433597968 ) ) ;
#3889=ORIENTED_EDGE ( 'NONE', *, *, #6847, .F. ) ;
#3907=AXIS2_PLACEMENT_3D ( 'NONE', #16665, #11681, #12885 ) ;
#3942=VECTOR ( 'NONE', #7402, 1000.000000000000000 ) ;
#3947=ADVANCED_FACE ( 'NONE', ( #8953 ), #12897, .F. ) ;
#3950=CARTESIAN_POINT ( 'NONE',  ( 0.000000000000000000, 451.4647406485092915, -149.8062676851188257 ) ) ;
#3961=DIRECTION ( 'NONE',  ( -1.000000000000000000, -0.000000000000000000, -0.000000000000000000 ) ) ;
#3971=EDGE_CURVE ( 'NONE', #16075, #6598, #15565, .T. ) ;
#4035=ORIENTED_EDGE ( 'NONE', *, *, #14351, .F. ) ;
#4050=ORIENTED_EDGE ( 'NONE', *, *, #15398, .T. ) ;
#4051=DIRECTION ( 'NONE',  ( 0.000000000000000000, -0.3746065934159093502, -0.9271838545667885345 ) ) ;
#4060=EDGE_CURVE ( 'NONE', #7330, #9826, #12988, .T. ) ;
#4152=ORIENTED_EDGE ( 'NONE', *, *, #15469, .T. ) ;
#4240=CARTESIAN_POINT ( 'NONE',  ( 0.000000000000000000, 240.7889724647196488, -16.41886574335980242 ) ) ;
#4242=CARTESIAN_POINT ( 'NONE',  ( 394.0000000000001137, 451.4647406485092915, -149.8062676851188257 ) ) ;
#4265=EDGE_CURVE ( 'NONE', #12820, #7289, #14003, .T. ) ;
#4315=PLANE ( 'NONE',  #8403 ) ;
#4323=PRODUCT_CONTEXT ( 'NONE', #13576, 'mechanical' ) ;
#4334=VERTEX_POINT ( 'NONE', #13924 ) ;
#4347=AXIS2_PLACEMENT_3D ( 'NONE', #10256, #14032, #8538 ) ;
#4348=FACE_OUTER_BOUND ( 'NONE', #5610, .T. ) ;
#4358=VECTOR ( 'NONE', #445, 1000.000000000000227 ) ;
#4398=ORIENTED_EDGE ( 'NONE', *, *, #13882, .T. ) ;
#4425=DIRECTION ( 'NONE',  ( -1.000000000000000000, 0.000000000000000000, 0.000000000000000000 ) ) ;
#4434=CARTESIAN_POINT ( 'NONE',  ( 394.0000000000001137, 339.4485271457189128, -10.62862937063367852 ) ) ;
#4457=LINE ( 'NONE', #9449, #7106 ) ;
#4494=ADVANCED_FACE ( 'NONE', ( #14776 ), #1547, .F. ) ;
#4496=ORIENTED_EDGE ( 'NONE', *, *, #15919, .F. ) ;
#4524=DIRECTION ( 'NONE',  ( 0.000000000000000000, -1.321694076934710402E-16, 1.000000000000000000 ) ) ;
#4526=EDGE_LOOP ( 'NONE', ( #15153, #9628, #11313, #8607 ) ) ;
#4544=ORIENTED_EDGE ( 'NONE', *, *, #2153, .T. ) ;
#4546=EDGE_CURVE ( 'NONE', #12299, #583, #433, .T. ) ;
#4565=AXIS2_PLACEMENT_3D ( 'NONE', #11648, #11554, #15347 ) ;
#4578=VECTOR ( 'NONE', #5007, 1000.000000000000000 ) ;
#4589=DIRECTION ( 'NONE',  ( -1.000000000000000000, -0.000000000000000000, -0.000000000000000000 ) ) ;
#4598=CARTESIAN_POINT ( 'NONE',  ( 394.0000000000001137, 240.7889724647196488, -104.2090657433598011 ) ) ;
#4633=CARTESIAN_POINT ( 'NONE',  ( 394.0000000000001137, 339.1725919290087745, -16.41886574335978821 ) ) ;
#4635=ORIENTED_EDGE ( 'NONE', *, *, #6528, .T. ) ;
#4730=DIRECTION ( 'NONE',  ( 0.000000000000000000, 0.000000000000000000, -1.000000000000000000 ) ) ;
#4782=CARTESIAN_POINT ( 'NONE',  ( 0.000000000000000000, 341.5974953295086038, -15.94751227074151956 ) ) ;
#4824=ADVANCED_FACE ( 'NONE', ( #4871 ), #1091, .T. ) ;
#4828=( LENGTH_UNIT ( ) NAMED_UNIT ( * ) SI_UNIT ( .MILLI., .METRE. ) );
#4859=EDGE_CURVE ( 'NONE', #1879, #2075, #12782, .T. ) ;
#4871=FACE_OUTER_BOUND ( 'NONE', #13857, .T. ) ;
#4880=EDGE_LOOP ( 'NONE', ( #14735, #12528, #2019, #13484 ) ) ;
#4909=( NAMED_UNIT ( * ) PLANE_ANGLE_UNIT ( ) SI_UNIT ( $, .RADIAN. ) );
#4919=DIRECTION ( 'NONE',  ( -1.000000000000000000, -0.000000000000000000, -0.000000000000000000 ) ) ;
#4938=CARTESIAN_POINT ( 'NONE',  ( 394.0000000000001137, 240.7889724647196488, -104.2090657433598011 ) ) ;
#5004=DIRECTION ( 'NONE',  ( 1.000000000000000000, 0.000000000000000000, 0.000000000000000000 ) ) ;
#5006=ORIENTED_EDGE ( 'NONE', *, *, #15310, .F. ) ;
#5007=DIRECTION ( 'NONE',  ( 0.000000000000000000, 0.000000000000000000, -1.000000000000000000 ) ) ;
#5041=VECTOR ( 'NONE', #11433, 1000.000000000000000 ) ;
#5067=ORIENTED_EDGE ( 'NONE', *, *, #16337, .F. ) ;
#5092=CARTESIAN_POINT ( 'NONE',  ( 394.0000000000001137, 240.0523724647196389, -17.15546574335979813 ) ) ;
#5114=PLANE ( 'NONE',  #4565 ) ;
#5127=CYLINDRICAL_SURFACE ( 'NONE', #12687, 0.7366000000000004766 ) ;
#5137=VERTEX_POINT ( 'NONE', #13641 ) ;
#5142=CARTESIAN_POINT ( 'NONE',  ( 394.0000000000001137, 240.7889724647196488, -17.15546574335979813 ) ) ;
#5153=CARTESIAN_POINT ( 'NONE',  ( 394.0000000000001137, 339.1725919290084335, -110.6822657433597925 ) ) ;
#5159=VECTOR ( 'NONE', #15539, 1000.000000000000227 ) ;
#5216=CIRCLE ( 'NONE', #11813, 0.7366000000000039183 ) ;
#5221=DIRECTION ( 'NONE',  ( 0.000000000000000000, 0.000000000000000000, -1.000000000000000000 ) ) ;
#5233=CARTESIAN_POINT ( 'NONE',  ( 0.000000000000000000, 240.0523724647196389, -110.6822657433598067 ) ) ;
#5241=LINE ( 'NONE', #8962, #6900 ) ;
#5243=ORIENTED_EDGE ( 'NONE', *, *, #22, .F. ) ;
#5281=VECTOR ( 'NONE', #2952, 1000.000000000000000 ) ;
#5313=ADVANCED_FACE ( 'NONE', ( #15254 ), #7415, .F. ) ;
#5335=EDGE_CURVE ( 'NONE', #3462, #12242, #11633, .T. ) ;
#5366=LINE ( 'NONE', #5712, #15462 ) ;
#5368=LINE ( 'NONE', #14745, #1933 ) ;
#5412=CARTESIAN_POINT ( 'NONE',  ( 394.0000000000001137, 451.4647406485094621, 28.44173619839933309 ) ) ;
#5415=ORIENTED_EDGE ( 'NONE', *, *, #9078, .T. ) ;
#5418=ORIENTED_EDGE ( 'NONE', *, *, #3834, .T. ) ;
#5455=LINE ( 'NONE', #8208, #10154 ) ;
#5479=VECTOR ( 'NONE', #3078, 999.9999999999998863 ) ;
#5480=EDGE_LOOP ( 'NONE', ( #106, #1025, #14897, #633 ) ) ;
#5488=CARTESIAN_POINT ( 'NONE',  ( 394.0000000000001137, 240.7889724647196488, -16.41886574335980242 ) ) ;
#5515=PLANE ( 'NONE',  #16797 ) ;
#5519=VERTEX_POINT ( 'NONE', #3044 ) ;
#5522=ADVANCED_FACE ( 'NONE', ( #13619 ), #12239, .F. ) ;
#5565=AXIS2_PLACEMENT_3D ( 'NONE', #3846, #9083, #14320 ) ;
#5572=DIRECTION ( 'NONE',  ( -1.000000000000000000, 0.000000000000000000, 0.000000000000000000 ) ) ;
#5578=PLANE ( 'NONE',  #2524 ) ;
#5594=VECTOR ( 'NONE', #7216, 1000.000000000000000 ) ;
#5610=EDGE_LOOP ( 'NONE', ( #1530, #2802, #7258, #1783 ) ) ;
#5614=FACE_OUTER_BOUND ( 'NONE', #9592, .T. ) ;
#5633=CYLINDRICAL_SURFACE ( 'NONE', #14501, 0.7366000000000004766 ) ;
#5642=LINE ( 'NONE', #1608, #2797 ) ;
#5661=CARTESIAN_POINT ( 'NONE',  ( 394.0000000000001137, 234.3157724647196289, -110.6822657433598067 ) ) ;
#5668=UNCERTAINTY_MEASURE_WITH_UNIT (LENGTH_MEASURE( 1.000000000000000082E-05 ), #4828, 'distance_accuracy_value', 'NONE');
#5688=DIRECTION ( 'NONE',  ( 1.000000000000000000, -0.000000000000000000, -0.000000000000000000 ) ) ;
#5691=PLANE ( 'NONE',  #14741 ) ;
#5712=CARTESIAN_POINT ( 'NONE',  ( 0.000000000000000000, 449.3157724647196005, -155.1251505852266632 ) ) ;
#5718=CARTESIAN_POINT ( 'NONE',  ( 394.0000000000001137, 449.3157724647197142, 33.76061909850716347 ) ) ;
#5730=ORIENTED_EDGE ( 'NONE', *, *, #13882, .F. ) ;
#5807=ORIENTED_EDGE ( 'NONE', *, *, #3876, .F. ) ;
#5834=CIRCLE ( 'NONE', #16262, 6.473199999999998511 ) ;
#5840=EDGE_CURVE ( 'NONE', #7396, #1879, #13912, .T. ) ;
#5847=VECTOR ( 'NONE', #10262, 1000.000000000000000 ) ;
#5859=EDGE_LOOP ( 'NONE', ( #11537, #10237, #10919, #10160 ) ) ;
#5872=LINE ( 'NONE', #11117, #15687 ) ;
#5880=FACE_OUTER_BOUND ( 'NONE', #7699, .T. ) ;
#5885=PRODUCT_DEFINITION_FORMATION_WITH_SPECIFIED_SOURCE ( 'ANY', '', #8239, .NOT_KNOWN. ) ;
#5966=CARTESIAN_POINT ( 'NONE',  ( 0.000000000000000000, 234.3157724647196289, -110.6822657433598067 ) ) ;
#5969=EDGE_CURVE ( 'NONE', #2075, #884, #1273, .T. ) ;
#5975=DIRECTION ( 'NONE',  ( 1.000000000000000000, -0.000000000000000000, -0.000000000000000000 ) ) ;
#6001=ORIENTED_EDGE ( 'NONE', *, *, #10017, .T. ) ;
#6006=VECTOR ( 'NONE', #9357, 1000.000000000000114 ) ;
#6026=AXIS2_PLACEMENT_3D ( 'NONE', #9236, #15911, #13445 ) ;
#6094=CARTESIAN_POINT ( 'NONE',  ( 394.0000000000001137, 449.3157724647196005, -155.1251505852266632 ) ) ;
#6097=PLANE ( 'NONE',  #6384 ) ;
#6123=ORIENTED_EDGE ( 'NONE', *, *, #2247, .F. ) ;
#6130=AXIS2_PLACEMENT_3D ( 'NONE', #2668, #4051, #10738 ) ;
#6181=ORIENTED_EDGE ( 'NONE', *, *, #7467, .T. ) ;
#6183=CARTESIAN_POINT ( 'NONE',  ( 394.0000000000001137, 451.4647406485092915, -149.8062676851188257 ) ) ;
#6271=CARTESIAN_POINT ( 'NONE',  ( 394.0000000000001137, 339.1725919290087745, -16.41886574335978821 ) ) ;
#6298=ADVANCED_FACE ( 'NONE', ( #11788 ), #10190, .T. ) ;
#6308=DIRECTION ( 'NONE',  ( 1.000000000000000000, 0.000000000000000000, -0.000000000000000000 ) ) ;
#6324=CIRCLE ( 'NONE', #9917, 0.7366000000000004766 ) ;
#6353=VECTOR ( 'NONE', #9770, 1000.000000000000000 ) ;
#6356=ORIENTED_EDGE ( 'NONE', *, *, #16337, .T. ) ;
#6357=DIRECTION ( 'NONE',  ( -1.000000000000000000, -0.000000000000000000, -0.000000000000000000 ) ) ;
#6366=CARTESIAN_POINT ( 'NONE',  ( 0.000000000000000000, 339.1725919290087745, -10.68226574335978718 ) ) ;
#6371=AXIS2_PLACEMENT_3D ( 'NONE', #14123, #2343, #11202 ) ;
#6384=AXIS2_PLACEMENT_3D ( 'NONE', #11347, #7555, #2585 ) ;
#6434=DIRECTION ( 'NONE',  ( 0.000000000000000000, 0.000000000000000000, 1.000000000000000000 ) ) ;
#6443=VECTOR ( 'NONE', #2435, 1000.000000000000000 ) ;
#6452=CARTESIAN_POINT ( 'NONE',  ( 394.0000000000001137, 451.4647406485092915, -149.8062676851188257 ) ) ;
#6472=FACE_OUTER_BOUND ( 'NONE', #5480, .T. ) ;
#6480=EDGE_LOOP ( 'NONE', ( #9458, #8091, #14807, #10373 ) ) ;
#6494=CARTESIAN_POINT ( 'NONE',  ( 394.0000000000001137, 339.3157724647196005, -110.6822657433597925 ) ) ;
#6528=EDGE_CURVE ( 'NONE', #4334, #9087, #1578, .T. ) ;
#6536=ADVANCED_FACE ( 'NONE', ( #13520 ), #5691, .T. ) ;
#6554=DIRECTION ( 'NONE',  ( -0.000000000000000000, 0.000000000000000000, -1.000000000000000000 ) ) ;
#6598=VERTEX_POINT ( 'NONE', #12638 ) ;
#6620=LINE ( 'NONE', #15650, #642 ) ;
#6623=CARTESIAN_POINT ( 'NONE',  ( 394.0000000000001137, 339.3157724647196005, -10.68226574335978718 ) ) ;
#6625=EDGE_CURVE ( 'NONE', #16672, #7289, #14101, .T. ) ;
#6635=CARTESIAN_POINT ( 'NONE',  ( 0.000000000000000000, 240.7889724647196488, -17.15546574335979813 ) ) ;
#6663=CARTESIAN_POINT ( 'NONE',  ( 394.0000000000001137, 240.0523724647196389, -104.2090657433598011 ) ) ;
#6670=CIRCLE ( 'NONE', #14370, 6.473200000000002063 ) ;
#6685=CARTESIAN_POINT ( 'NONE',  ( 0.000000000000000000, 339.4485271457185718, -110.7359021160857537 ) ) ;
#6695=CARTESIAN_POINT ( 'NONE',  ( 0.000000000000000000, 240.7889724647196488, -104.9456657433598110 ) ) ;
#6732=DIRECTION ( 'NONE',  ( -1.000000000000000000, -0.000000000000000000, -0.000000000000000000 ) ) ;
#6741=DIRECTION ( 'NONE',  ( 0.000000000000000000, 0.9271838545667883125, 0.3746065934159095168 ) ) ;
#6748=DIRECTION ( 'NONE',  ( -1.000000000000000000, -0.000000000000000000, -0.000000000000000000 ) ) ;
#6772=AXIS2_PLACEMENT_3D ( 'NONE', #13525, #9657, #12234 ) ;
#6774=CARTESIAN_POINT ( 'NONE',  ( 394.0000000000001137, 339.3157724647196005, -10.68226574335978718 ) ) ;
#6791=ORIENTED_EDGE ( 'NONE', *, *, #2895, .T. ) ;
#6808=ORIENTED_EDGE ( 'NONE', *, *, #5335, .T. ) ;
#6847=EDGE_CURVE ( 'NONE', #13380, #884, #101, .T. ) ;
#6849=CARTESIAN_POINT ( 'NONE',  ( 0.000000000000000000, 240.7889724647196488, -16.41886574335980242 ) ) ;
#6858=DIRECTION ( 'NONE',  ( 0.000000000000000000, 1.321694076934710402E-16, -1.000000000000000000 ) ) ;
#6871=ADVANCED_FACE ( 'NONE', ( #446 ), #13334, .T. ) ;
#6894=EDGE_CURVE ( 'NONE', #8784, #6948, #2933, .T. ) ;
#6898=CARTESIAN_POINT ( 'NONE',  ( 0.000000000000000000, 339.1725919290087745, -9.945665743359786148 ) ) ;
#6900=VECTOR ( 'NONE', #10496, 1000.000000000000000 ) ;
#6916=DIRECTION ( 'NONE',  ( 0.000000000000000000, 1.000000000000000000, 1.321694076934710402E-16 ) ) ;
#6920=PLANE ( 'NONE',  #15171 ) ;
#6938=VECTOR ( 'NONE', #12052, 1000.000000000000000 ) ;
#6946=ADVANCED_FACE ( 'NONE', ( #11000 ), #4315, .T. ) ;
#6948=VERTEX_POINT ( 'NONE', #6951 ) ;
#6951=CARTESIAN_POINT ( 'NONE',  ( 0.000000000000000000, 240.7889724647196488, -16.41886574335980242 ) ) ;
#6969=EDGE_CURVE ( 'NONE', #6598, #3462, #8335, .T. ) ;
#6971=CARTESIAN_POINT ( 'NONE',  ( 0.000000000000000000, 339.4485271457185718, -110.7359021160857537 ) ) ;
#7003=DIRECTION ( 'NONE',  ( -1.000000000000000000, -0.000000000000000000, -0.000000000000000000 ) ) ;
#7029=EDGE_CURVE ( 'NONE', #16672, #12012, #3602, .T. ) ;
#7098=DIRECTION ( 'NONE',  ( 0.000000000000000000, 0.000000000000000000, 1.000000000000000000 ) ) ;
#7106=VECTOR ( 'NONE', #13323, 1000.000000000000000 ) ;
#7137=ORIENTED_EDGE ( 'NONE', *, *, #13970, .T. ) ;
#7143=DIRECTION ( 'NONE',  ( 1.000000000000000000, 0.000000000000000000, -0.000000000000000000 ) ) ;
#7167=CIRCLE ( 'NONE', #7448, 0.7366000000000039183 ) ;
#7194=VECTOR ( 'NONE', #10094, 1000.000000000000114 ) ;
#7216=DIRECTION ( 'NONE',  ( -1.000000000000000000, -0.000000000000000000, -0.000000000000000000 ) ) ;
#7223=DIRECTION ( 'NONE',  ( 1.000000000000000000, 0.000000000000000000, 0.000000000000000000 ) ) ;
#7229=( NAMED_UNIT ( * ) SI_UNIT ( $, .STERADIAN. ) SOLID_ANGLE_UNIT ( ) );
#7233=DIRECTION ( 'NONE',  ( 0.000000000000000000, -1.000000000000000000, 0.000000000000000000 ) ) ;
#7235=PLANE ( 'NONE',  #10729 ) ;
#7239=FACE_OUTER_BOUND ( 'NONE', #2929, .T. ) ;
#7246=DIRECTION ( 'NONE',  ( 0.000000000000000000, 0.000000000000000000, -1.000000000000000000 ) ) ;
#7248=FACE_OUTER_BOUND ( 'NONE', #13969, .T. ) ;
#7258=ORIENTED_EDGE ( 'NONE', *, *, #4859, .T. ) ;
#7289=VERTEX_POINT ( 'NONE', #2729 ) ;
#7307=ORIENTED_EDGE ( 'NONE', *, *, #16539, .F. ) ;
#7330=VERTEX_POINT ( 'NONE', #10810 ) ;
#7345=ORIENTED_EDGE ( 'NONE', *, *, #13170, .F. ) ;
#7372=EDGE_LOOP ( 'NONE', ( #8978, #6181, #11548, #7992 ) ) ;
#7373=ORIENTED_EDGE ( 'NONE', *, *, #2555, .T. ) ;
#7396=VERTEX_POINT ( 'NONE', #4782 ) ;
#7401=LINE ( 'NONE', #813, #12924 ) ;
#7402=DIRECTION ( 'NONE',  ( 0.000000000000000000, -1.000000000000000000, -1.321694076934710402E-16 ) ) ;
#7415=PLANE ( 'NONE',  #13875 ) ;
#7424=DIRECTION ( 'NONE',  ( -1.000000000000000000, -0.000000000000000000, -0.000000000000000000 ) ) ;
#7432=AXIS2_PLACEMENT_3D ( 'NONE', #7995, #12134, #1485 ) ;
#7448=AXIS2_PLACEMENT_3D ( 'NONE', #11996, #406, #1779 ) ;
#7452=DIRECTION ( 'NONE',  ( 0.000000000000000000, -0.9271838545667883125, -0.3746065934159094613 ) ) ;
#7467=EDGE_CURVE ( 'NONE', #49, #12012, #16897, .T. ) ;
#7498=DIRECTION ( 'NONE',  ( 0.000000000000000000, -0.3746065934159049648, -0.9271838545667903109 ) ) ;
#7504=EDGE_LOOP ( 'NONE', ( #14793, #5006, #11113, #11625 ) ) ;
#7515=ORIENTED_EDGE ( 'NONE', *, *, #7029, .F. ) ;
#7526=EDGE_CURVE ( 'NONE', #583, #49, #1010, .T. ) ;
#7555=DIRECTION ( 'NONE',  ( -1.000000000000000000, 0.000000000000000000, 0.000000000000000000 ) ) ;
#7579=LINE ( 'NONE', #6366, #4578 ) ;
#7580=DIRECTION ( 'NONE',  ( -0.000000000000000000, 0.000000000000000000, -1.000000000000000000 ) ) ;
#7582=ADVANCED_FACE ( 'NONE', ( #1084 ), #5114, .T. ) ;
#7584=LINE ( 'NONE', #16941, #11525 ) ;
#7656=CARTESIAN_POINT ( 'NONE',  ( 394.0000000000001137, 240.0523724647196389, -17.15546574335979813 ) ) ;
#7689=FACE_OUTER_BOUND ( 'NONE', #9336, .T. ) ;
#7693=DIRECTION ( 'NONE',  ( 0.000000000000000000, 0.3746065934159141242, -0.9271838545667866471 ) ) ;
#7699=EDGE_LOOP ( 'NONE', ( #35, #6808, #14273, #6356 ) ) ;
#7706=ADVANCED_BREP_SHAPE_REPRESENTATION ( '', ( #3164, #1488 ), #16580 ) ;
#7723=ORIENTED_EDGE ( 'NONE', *, *, #9875, .F. ) ;
#7743=AXIS2_PLACEMENT_3D ( 'NONE', #13386, #159, #1611 ) ;
#7770=CIRCLE ( 'NONE', #676, 0.7366000000000004766 ) ;
#7788=FACE_OUTER_BOUND ( 'NONE', #7820, .T. ) ;
#7820=EDGE_LOOP ( 'NONE', ( #4496, #15723, #1345, #14814 ) ) ;
#7825=VECTOR ( 'NONE', #11017, 1000.000000000000227 ) ;
#7853=DIRECTION ( 'NONE',  ( 1.000000000000000000, 0.000000000000000000, -0.000000000000000000 ) ) ;
#7899=FACE_OUTER_BOUND ( 'NONE', #10475, .T. ) ;
#7917=DIRECTION ( 'NONE',  ( -1.000000000000000000, -0.000000000000000000, -0.000000000000000000 ) ) ;
#7927=VERTEX_POINT ( 'NONE', #5092 ) ;
#7992=ORIENTED_EDGE ( 'NONE', *, *, #10017, .F. ) ;
#7995=CARTESIAN_POINT ( 'NONE',  ( 394.0000000000001137, 240.7889724647196488, -17.15546574335979813 ) ) ;
#8002=AXIS2_PLACEMENT_3D ( 'NONE', #5142, #3961, #5221 ) ;
#8036=VERTEX_POINT ( 'NONE', #2429 ) ;
#8038=AXIS2_PLACEMENT_3D ( 'NONE', #14225, #7853, #6554 ) ;
#8048=EDGE_CURVE ( 'NONE', #15132, #14037, #7579, .T. ) ;
#8058=CIRCLE ( 'NONE', #13831, 0.7366000000000004766 ) ;
#8069=VECTOR ( 'NONE', #10490, 1000.000000000000000 ) ;
#8091=ORIENTED_EDGE ( 'NONE', *, *, #2606, .F. ) ;
#8093=ORIENTED_EDGE ( 'NONE', *, *, #10955, .F. ) ;
#8124=CARTESIAN_POINT ( 'NONE',  ( 394.0000000000001137, 339.1725919290087745, -9.945665743359786148 ) ) ;
#8131=ORIENTED_EDGE ( 'NONE', *, *, #2037, .T. ) ;
#8134=VECTOR ( 'NONE', #2448, 1000.000000000000000 ) ;
#8138=CYLINDRICAL_SURFACE ( 'NONE', #7743, 6.473199999999998511 ) ;
#8159=FACE_OUTER_BOUND ( 'NONE', #3039, .T. ) ;
#8201=CARTESIAN_POINT ( 'NONE',  ( 394.0000000000001137, 339.4485271457189128, -10.62862937063367852 ) ) ;
#8208=CARTESIAN_POINT ( 'NONE',  ( 394.0000000000001137, 240.7889724647196488, -10.68226574335980139 ) ) ;
#8239=PRODUCT ( 'Part8', 'Part8', '', ( #4323 ) ) ;
#8240=UNCERTAINTY_MEASURE_WITH_UNIT (LENGTH_MEASURE( 1.000000000000000082E-05 ), #11087, 'distance_accuracy_value', 'NONE');
#8242=LINE ( 'NONE', #11143, #13308 ) ;
#8249=DIRECTION ( 'NONE',  ( -0.000000000000000000, 0.9271838545667866471, 0.3746065934159141242 ) ) ;
#8267=CARTESIAN_POINT ( 'NONE',  ( 394.0000000000001137, 449.3157724647196005, -155.1251505852266632 ) ) ;
#8273=ORIENTED_EDGE ( 'NONE', *, *, #16025, .F. ) ;
#8276=DIRECTION ( 'NONE',  ( 0.000000000000000000, -1.000000000000000000, 0.000000000000000000 ) ) ;
#8279=ORIENTED_EDGE ( 'NONE', *, *, #1960, .F. ) ;
#8281=DIRECTION ( 'NONE',  ( -0.000000000000000000, 0.000000000000000000, -1.000000000000000000 ) ) ;
#8284=VECTOR ( 'NONE', #6357, 1000.000000000000000 ) ;
#8316=AXIS2_PLACEMENT_3D ( 'NONE', #8975, #11713, #7580 ) ;
#8327=ORIENTED_EDGE ( 'NONE', *, *, #10761, .F. ) ;
#8335=LINE ( 'NONE', #9461, #11683 ) ;
#8341=EDGE_CURVE ( 'NONE', #3462, #3010, #13926, .T. ) ;
#8372=ORIENTED_EDGE ( 'NONE', *, *, #2555, .F. ) ;
#8390=DIRECTION ( 'NONE',  ( 0.000000000000000000, 0.000000000000000000, 1.000000000000000000 ) ) ;
#8403=AXIS2_PLACEMENT_3D ( 'NONE', #3102, #357, #9549 ) ;
#8404=EDGE_LOOP ( 'NONE', ( #7345, #7723, #7307, #4050 ) ) ;
#8453=ORIENTED_EDGE ( 'NONE', *, *, #6847, .T. ) ;
#8458=DIRECTION ( 'NONE',  ( -1.000000000000000000, 0.000000000000000000, 0.000000000000000000 ) ) ;
#8486=CARTESIAN_POINT ( 'NONE',  ( 394.0000000000001137, 339.1725919290087745, -16.41886574335978821 ) ) ;
#8491=CARTESIAN_POINT ( 'NONE',  ( 0.000000000000000000, 240.7889724647196488, -110.6822657433598067 ) ) ;
#8534=ORIENTED_EDGE ( 'NONE', *, *, #808, .F. ) ;
#8535=PLANE ( 'NONE',  #15424 ) ;
#8538=DIRECTION ( 'NONE',  ( 0.000000000000000000, 0.000000000000000000, 1.000000000000000000 ) ) ;
#8592=VECTOR ( 'NONE', #14380, 1000.000000000000114 ) ;
#8607=ORIENTED_EDGE ( 'NONE', *, *, #9636, .T. ) ;
#8621=VECTOR ( 'NONE', #9683, 1000.000000000000000 ) ;
#8676=ORIENTED_EDGE ( 'NONE', *, *, #9078, .F. ) ;
#8681=ORIENTED_EDGE ( 'NONE', *, *, #13395, .T. ) ;
#8693=DIRECTION ( 'NONE',  ( 0.000000000000000000, 0.000000000000000000, 1.000000000000000000 ) ) ;
#8697=AXIS2_PLACEMENT_3D ( 'NONE', #4938, #7424, #15426 ) ;
#8722=CARTESIAN_POINT ( 'NONE',  ( 394.0000000000001137, 240.7889724647196488, -110.6822657433598067 ) ) ;
#8732=AXIS2_PLACEMENT_3D ( 'NONE', #15883, #6858, #14607 ) ;
#8784=VERTEX_POINT ( 'NONE', #1089 ) ;
#8804=AXIS2_PLACEMENT_3D ( 'NONE', #12588, #914, #16699 ) ;
#8811=CARTESIAN_POINT ( 'NONE',  ( 394.0000000000001137, 341.5974953295075807, -105.4170192159777031 ) ) ;
#8835=VECTOR ( 'NONE', #12026, 1000.000000000000000 ) ;
#8860=CARTESIAN_POINT ( 'NONE',  ( 394.0000000000001137, 240.7889724647196488, -104.2090657433598011 ) ) ;
#8878=DIRECTION ( 'NONE',  ( -1.000000000000000000, 0.000000000000000000, 0.000000000000000000 ) ) ;
#8881=VECTOR ( 'NONE', #10363, 1000.000000000000114 ) ;
#8884=PLANE ( 'NONE',  #6371 ) ;
#8889=EDGE_CURVE ( 'NONE', #16672, #8784, #5455, .T. ) ;
#8903=VECTOR ( 'NONE', #543, 1000.000000000000000 ) ;
#8953=FACE_OUTER_BOUND ( 'NONE', #4526, .T. ) ;
#8962=CARTESIAN_POINT ( 'NONE',  ( 0.000000000000000000, 240.0523724647196389, -104.2090657433598011 ) ) ;
#8975=CARTESIAN_POINT ( 'NONE',  ( 394.0000000000001137, 240.7889724647196488, -10.68226574335980139 ) ) ;
#8978=ORIENTED_EDGE ( 'NONE', *, *, #16537, .F. ) ;
#8987=ADVANCED_FACE ( 'NONE', ( #7248 ), #16616, .F. ) ;
#8988=DIRECTION ( 'NONE',  ( 0.000000000000000000, -1.000000000000000000, -1.321694076934710402E-16 ) ) ;
#8994=ORIENTED_EDGE ( 'NONE', *, *, #6969, .F. ) ;
#9002=EDGE_LOOP ( 'NONE', ( #2433, #3652, #10356, #14510 ) ) ;
#9027=CARTESIAN_POINT ( 'NONE',  ( 394.0000000000001137, 339.3157724647196005, -16.41886574335978821 ) ) ;
#9044=EDGE_LOOP ( 'NONE', ( #8994, #14736, #187, #8681 ) ) ;
#9076=ORIENTED_EDGE ( 'NONE', *, *, #2476, .T. ) ;
#9078=EDGE_CURVE ( 'NONE', #12512, #4334, #7584, .T. ) ;
#9083=DIRECTION ( 'NONE',  ( -1.000000000000000000, 0.000000000000000000, 0.000000000000000000 ) ) ;
#9087=VERTEX_POINT ( 'NONE', #16775 ) ;
#9142=LINE ( 'NONE', #6452, #8592 ) ;
#9207=ADVANCED_FACE ( 'NONE', ( #5614 ), #9396, .T. ) ;
#9208=FACE_OUTER_BOUND ( 'NONE', #9044, .T. ) ;
#9236=CARTESIAN_POINT ( 'NONE',  ( 394.0000000000001137, 449.3157724647196005, -155.1251505852266632 ) ) ;
#9335=ORIENTED_EDGE ( 'NONE', *, *, #7526, .F. ) ;
#9336=EDGE_LOOP ( 'NONE', ( #774, #15089, #5067, #8372 ) ) ;
#9338=LINE ( 'NONE', #6663, #56 ) ;
#9340=FACE_OUTER_BOUND ( 'NONE', #15106, .T. ) ;
#9353=VECTOR ( 'NONE', #12087, 1000.000000000000000 ) ;
#9357=DIRECTION ( 'NONE',  ( 0.000000000000000000, 0.3746065934157932764, 0.9271838545668352749 ) ) ;
#9370=CLOSED_SHELL ( 'NONE', ( #6946, #11567, #14856, #10272, #9799, #14309, #7582, #13300, #791, #16506, #10450, #13699, #4824, #10452, #12035, #918, #1096, #6871, #10895, #2262, #1020, #10555, #14928, #6298, #1856, #285, #9207, #6536, #3056, #14977, #5313, #3947, #5522, #11281, #8987, #1752, #4494, #10124 ) ) ;
#9396=PLANE ( 'NONE',  #6026 ) ;
#9446=DIRECTION ( 'NONE',  ( 0.000000000000000000, 0.000000000000000000, 1.000000000000000000 ) ) ;
#9449=CARTESIAN_POINT ( 'NONE',  ( 394.0000000000001137, 449.3157724647197142, 33.76061909850716347 ) ) ;
#9458=ORIENTED_EDGE ( 'NONE', *, *, #4060, .T. ) ;
#9461=CARTESIAN_POINT ( 'NONE',  ( 0.000000000000000000, 339.3157724647196005, -110.6822657433597925 ) ) ;
#9512=EDGE_LOOP ( 'NONE', ( #13891, #7515, #14580, #1033 ) ) ;
#9549=DIRECTION ( 'NONE',  ( -0.000000000000000000, 0.000000000000000000, -1.000000000000000000 ) ) ;
#9560=ORIENTED_EDGE ( 'NONE', *, *, #5969, .F. ) ;
#9580=DIRECTION ( 'NONE',  ( 0.000000000000000000, 0.000000000000000000, 1.000000000000000000 ) ) ;
#9592=EDGE_LOOP ( 'NONE', ( #1822, #8273, #4635, #14295 ) ) ;
#9624=DIRECTION ( 'NONE',  ( 0.000000000000000000, -0.3746065934159096833, 0.9271838545667884235 ) ) ;
#9628=ORIENTED_EDGE ( 'NONE', *, *, #14006, .F. ) ;
#9636=EDGE_CURVE ( 'NONE', #11171, #12242, #2901, .T. ) ;
#9653=EDGE_LOOP ( 'NONE', ( #7373, #3248, #13172, #12807 ) ) ;
#9657=DIRECTION ( 'NONE',  ( -1.000000000000000000, -0.000000000000000000, -0.000000000000000000 ) ) ;
#9673=CIRCLE ( 'NONE', #3907, 0.7366000000000039183 ) ;
#9683=DIRECTION ( 'NONE',  ( -1.000000000000000000, -0.000000000000000000, -0.000000000000000000 ) ) ;
#9701=AXIS2_PLACEMENT_3D ( 'NONE', #10136, #863, #7452 ) ;
#9718=ORIENTED_EDGE ( 'NONE', *, *, #700, .F. ) ;
#9721=LINE ( 'NONE', #11242, #4358 ) ;
#9754=ORIENTED_EDGE ( 'NONE', *, *, #1200, .F. ) ;
#9770=DIRECTION ( 'NONE',  ( 0.000000000000000000, 0.000000000000000000, 1.000000000000000000 ) ) ;
#9772=CARTESIAN_POINT ( 'NONE',  ( 394.0000000000001137, 240.7889724647196488, -17.15546574335979813 ) ) ;
#9799=ADVANCED_FACE ( 'NONE', ( #755 ), #16377, .T. ) ;
#9808=FILL_AREA_STYLE ('',( #1893 ) ) ;
#9815=VERTEX_POINT ( 'NONE', #8811 ) ;
#9826=VERTEX_POINT ( 'NONE', #3664 ) ;
#9875=EDGE_CURVE ( 'NONE', #9087, #16075, #5216, .T. ) ;
#9887=DIRECTION ( 'NONE',  ( 0.000000000000000000, 0.000000000000000000, 1.000000000000000000 ) ) ;
#9903=ORIENTED_EDGE ( 'NONE', *, *, #3834, .F. ) ;
#9917=AXIS2_PLACEMENT_3D ( 'NONE', #6635, #3750, #11897 ) ;
#9996=ORIENTED_EDGE ( 'NONE', *, *, #808, .T. ) ;
#10017=EDGE_CURVE ( 'NONE', #9826, #6948, #6324, .T. ) ;
#10041=VECTOR ( 'NONE', #15387, 1000.000000000000000 ) ;
#10094=DIRECTION ( 'NONE',  ( 0.000000000000000000, -0.9271838545667884235, 0.3746065934159092392 ) ) ;
#10111=AXIS2_PLACEMENT_3D ( 'NONE', #16477, #12371, #11167 ) ;
#10117=DIRECTION ( 'NONE',  ( -0.000000000000000000, 0.000000000000000000, -1.000000000000000000 ) ) ;
#10124=ADVANCED_FACE ( 'NONE', ( #4348 ), #13452, .T. ) ;
#10136=CARTESIAN_POINT ( 'NONE',  ( 394.0000000000001137, 341.4647406485092915, -16.00114864346762644 ) ) ;
#10137=ORIENTED_EDGE ( 'NONE', *, *, #6894, .T. ) ;
#10154=VECTOR ( 'NONE', #494, 1000.000000000000000 ) ;
#10160=ORIENTED_EDGE ( 'NONE', *, *, #1200, .T. ) ;
#10166=CYLINDRICAL_SURFACE ( 'NONE', #4347, 6.473200000000000287 ) ;
#10190=CYLINDRICAL_SURFACE ( 'NONE', #8697, 6.473199999999998511 ) ;
#10207=CARTESIAN_POINT ( 'NONE',  ( 394.0000000000001137, 240.7889724647196488, -104.9456657433598110 ) ) ;
#10222=VECTOR ( 'NONE', #1442, 1000.000000000000000 ) ;
#10237=ORIENTED_EDGE ( 'NONE', *, *, #13513, .T. ) ;
#10246=EDGE_CURVE ( 'NONE', #9815, #5137, #7401, .T. ) ;
#10256=CARTESIAN_POINT ( 'NONE',  ( 394.0000000000001137, 339.1725919290087745, -9.945665743359786148 ) ) ;
#10262=DIRECTION ( 'NONE',  ( -1.000000000000000000, -0.000000000000000000, -0.000000000000000000 ) ) ;
#10270=ORIENTED_EDGE ( 'NONE', *, *, #2677, .F. ) ;
#10272=ADVANCED_FACE ( 'NONE', ( #891 ), #7235, .T. ) ;
#10287=AXIS2_PLACEMENT_3D ( 'NONE', #11812, #3668, #2625 ) ;
#10294=DIRECTION ( 'NONE',  ( 0.000000000000000000, 0.9271838545667883125, 0.3746065934159095168 ) ) ;
#10299=CARTESIAN_POINT ( 'NONE',  ( 0.000000000000000000, 449.3157724647197142, 33.76061909850716347 ) ) ;
#10325=ORIENTED_EDGE ( 'NONE', *, *, #4060, .F. ) ;
#10336=PLANE ( 'NONE',  #10746 ) ;
#10344=VECTOR ( 'NONE', #12210, 1000.000000000000000 ) ;
#10356=ORIENTED_EDGE ( 'NONE', *, *, #10442, .F. ) ;
#10358=EDGE_CURVE ( 'NONE', #1644, #1233, #15733, .T. ) ;
#10363=DIRECTION ( 'NONE',  ( 0.000000000000000000, -0.3746065934157932764, -0.9271838545668352749 ) ) ;
#10373=ORIENTED_EDGE ( 'NONE', *, *, #14006, .T. ) ;
#10377=PLANE ( 'NONE',  #5565 ) ;
#10414=AXIS2_PLACEMENT_3D ( 'NONE', #12503, #4524, #824 ) ;
#10442=EDGE_CURVE ( 'NONE', #7330, #3010, #5241, .T. ) ;
#10450=ADVANCED_FACE ( 'NONE', ( #3640 ), #10336, .T. ) ;
#10452=ADVANCED_FACE ( 'NONE', ( #14118 ), #2339, .T. ) ;
#10475=EDGE_LOOP ( 'NONE', ( #14181, #15619, #8534, #12315 ) ) ;
#10490=DIRECTION ( 'NONE',  ( -0.000000000000000000, -0.000000000000000000, 1.000000000000000000 ) ) ;
#10496=DIRECTION ( 'NONE',  ( 0.000000000000000000, -1.000000000000000000, 0.000000000000000000 ) ) ;
#10525=CARTESIAN_POINT ( 'NONE',  ( 394.0000000000001137, 341.5974953295075807, -105.4170192159777031 ) ) ;
#10542=EDGE_LOOP ( 'NONE', ( #10270, #10683, #8093, #14715 ) ) ;
#10555=ADVANCED_FACE ( 'NONE', ( #2764 ), #14621, .T. ) ;
#10609=DIRECTION ( 'NONE',  ( 1.000000000000000000, 0.000000000000000000, 0.000000000000000000 ) ) ;
#10683=ORIENTED_EDGE ( 'NONE', *, *, #696, .F. ) ;
#10729=AXIS2_PLACEMENT_3D ( 'NONE', #15399, #8458, #3472 ) ;
#10738=DIRECTION ( 'NONE',  ( 0.000000000000000000, 0.9271838545667884235, -0.3746065934159092947 ) ) ;
#10742=EDGE_CURVE ( 'NONE', #12242, #7330, #9673, .T. ) ;
#10746=AXIS2_PLACEMENT_3D ( 'NONE', #1057, #8878, #12903 ) ;
#10761=EDGE_CURVE ( 'NONE', #583, #16672, #16781, .T. ) ;
#10810=CARTESIAN_POINT ( 'NONE',  ( 0.000000000000000000, 240.0523724647196389, -104.2090657433598011 ) ) ;
#10821=DIRECTION ( 'NONE',  ( 0.000000000000000000, 0.000000000000000000, 1.000000000000000000 ) ) ;
#10895=ADVANCED_FACE ( 'NONE', ( #3007 ), #5578, .T. ) ;
#10896=LINE ( 'NONE', #163, #10222 ) ;
#10918=DIRECTION ( 'NONE',  ( 0.000000000000000000, -0.3746065934159141242, 0.9271838545667866471 ) ) ;
#10919=ORIENTED_EDGE ( 'NONE', *, *, #770, .F. ) ;
#10920=CARTESIAN_POINT ( 'NONE',  ( 0.000000000000000000, 234.3157724647196289, -104.2090657433598011 ) ) ;
#10932=DIRECTION ( 'NONE',  ( 0.000000000000000000, 0.000000000000000000, 1.000000000000000000 ) ) ;
#10937=ORIENTED_EDGE ( 'NONE', *, *, #6894, .F. ) ;
#10946=CARTESIAN_POINT ( 'NONE',  ( 394.0000000000001137, 240.0523724647196389, -110.6822657433598067 ) ) ;
#10955=EDGE_CURVE ( 'NONE', #11171, #1365, #1715, .T. ) ;
#11000=FACE_OUTER_BOUND ( 'NONE', #8404, .T. ) ;
#11017=DIRECTION ( 'NONE',  ( 0.000000000000000000, -0.9271838545667884235, 0.3746065934159092392 ) ) ;
#11087=( LENGTH_UNIT ( ) NAMED_UNIT ( * ) SI_UNIT ( .MILLI., .METRE. ) );
#11106=CIRCLE ( 'NONE', #10287, 0.7366000000000004766 ) ;
#11113=ORIENTED_EDGE ( 'NONE', *, *, #9875, .T. ) ;
#11117=CARTESIAN_POINT ( 'NONE',  ( 394.0000000000001137, 240.0523724647196389, -17.15546574335979813 ) ) ;
#11125=ORIENTED_EDGE ( 'NONE', *, *, #15988, .F. ) ;
#11143=CARTESIAN_POINT ( 'NONE',  ( 0.000000000000000000, 339.1725919290084335, -104.9456657433597968 ) ) ;
#11167=DIRECTION ( 'NONE',  ( 0.000000000000000000, 0.000000000000000000, -1.000000000000000000 ) ) ;
#11171=VERTEX_POINT ( 'NONE', #10207 ) ;
#11202=DIRECTION ( 'NONE',  ( -0.000000000000000000, 0.000000000000000000, -1.000000000000000000 ) ) ;
#11222=PRODUCT_DEFINITION_CONTEXT ( 'detailed design', #2147, 'design' ) ;
#11242=CARTESIAN_POINT ( 'NONE',  ( 0.000000000000000000, 341.4647406485092915, -16.00114864346762644 ) ) ;
#11281=ADVANCED_FACE ( 'NONE', ( #3850 ), #5127, .F. ) ;
#11303=EDGE_CURVE ( 'NONE', #1082, #7927, #10896, .T. ) ;
#11308=DIRECTION ( 'NONE',  ( -1.000000000000000000, -0.000000000000000000, -0.000000000000000000 ) ) ;
#11313=ORIENTED_EDGE ( 'NONE', *, *, #11927, .F. ) ;
#11347=CARTESIAN_POINT ( 'NONE',  ( 0.000000000000000000, 339.1725919290087745, -10.68226574335978718 ) ) ;
#11390=EDGE_LOOP ( 'NONE', ( #1271, #9335, #15315, #16281 ) ) ;
#11413=CARTESIAN_POINT ( 'NONE',  ( 394.0000000000001137, 240.7889724647196488, -17.15546574335979813 ) ) ;
#11433=DIRECTION ( 'NONE',  ( -1.000000000000000000, -0.000000000000000000, -0.000000000000000000 ) ) ;
#11435=DIRECTION ( 'NONE',  ( -1.000000000000000000, -0.000000000000000000, -0.000000000000000000 ) ) ;
#11462=DIRECTION ( 'NONE',  ( 0.000000000000000000, 1.321694076934710402E-16, -1.000000000000000000 ) ) ;
#11482=CARTESIAN_POINT ( 'NONE',  ( 0.000000000000000000, 339.3157724647196005, -10.68226574335978718 ) ) ;
#11499=( NAMED_UNIT ( * ) SI_UNIT ( $, .STERADIAN. ) SOLID_ANGLE_UNIT ( ) );
#11525=VECTOR ( 'NONE', #7498, 1000.000000000000000 ) ;
#11533=CARTESIAN_POINT ( 'NONE',  ( 0.000000000000000000, 339.1725919290084335, -111.4188657433597456 ) ) ;
#11537=ORIENTED_EDGE ( 'NONE', *, *, #16704, .T. ) ;
#11548=ORIENTED_EDGE ( 'NONE', *, *, #11865, .F. ) ;
#11554=DIRECTION ( 'NONE',  ( -1.000000000000000000, 0.000000000000000000, 0.000000000000000000 ) ) ;
#11567=ADVANCED_FACE ( 'NONE', ( #7239 ), #8884, .T. ) ;
#11577=VECTOR ( 'NONE', #6741, 1000.000000000000114 ) ;
#11593=CARTESIAN_POINT ( 'NONE',  ( 394.0000000000001137, 339.1725919290084335, -110.6822657433597925 ) ) ;
#11625=ORIENTED_EDGE ( 'NONE', *, *, #3971, .T. ) ;
#11627=LINE ( 'NONE', #2430, #15170 ) ;
#11633=LINE ( 'NONE', #14216, #6443 ) ;
#11648=CARTESIAN_POINT ( 'NONE',  ( 0.000000000000000000, 240.7889724647196488, -110.6822657433598067 ) ) ;
#11650=VECTOR ( 'NONE', #9446, 1000.000000000000000 ) ;
#11657=LINE ( 'NONE', #15439, #15946 ) ;
#11671=CARTESIAN_POINT ( 'NONE',  ( 0.000000000000000000, 339.1725919290084335, -104.9456657433597968 ) ) ;
#11681=DIRECTION ( 'NONE',  ( -1.000000000000000000, -0.000000000000000000, -0.000000000000000000 ) ) ;
#11683=VECTOR ( 'NONE', #13587, 1000.000000000000000 ) ;
#11695=DIRECTION ( 'NONE',  ( -1.000000000000000000, -0.000000000000000000, -0.000000000000000000 ) ) ;
#11713=DIRECTION ( 'NONE',  ( 1.000000000000000000, 0.000000000000000000, -0.000000000000000000 ) ) ;
#11729=PLANE ( 'NONE',  #8038 ) ;
#11760=CIRCLE ( 'NONE', #10111, 6.473200000000002063 ) ;
#11776=VERTEX_POINT ( 'NONE', #6971 ) ;
#11788=FACE_OUTER_BOUND ( 'NONE', #1825, .T. ) ;
#11812=CARTESIAN_POINT ( 'NONE',  ( 394.0000000000001137, 339.1725919290087745, -9.945665743359786148 ) ) ;
#11813=AXIS2_PLACEMENT_3D ( 'NONE', #1001, #5975, #2278 ) ;
#11822=AXIS2_PLACEMENT_3D ( 'NONE', #6898, #4425, #9580 ) ;
#11865=EDGE_CURVE ( 'NONE', #6948, #12012, #13350, .T. ) ;
#11886=DIRECTION ( 'NONE',  ( 0.000000000000000000, -1.321694076934710402E-16, 1.000000000000000000 ) ) ;
#11895=VECTOR ( 'NONE', #2709, 1000.000000000000000 ) ;
#11897=DIRECTION ( 'NONE',  ( 0.000000000000000000, 0.000000000000000000, -1.000000000000000000 ) ) ;
#11907=CARTESIAN_POINT ( 'NONE',  ( 394.0000000000001137, 234.3157724647196289, -17.15546574335979813 ) ) ;
#11927=EDGE_CURVE ( 'NONE', #11171, #1082, #13820, .T. ) ;
#11938=EDGE_CURVE ( 'NONE', #12512, #8036, #15307, .T. ) ;
#11996=CARTESIAN_POINT ( 'NONE',  ( 0.000000000000000000, 339.1725919290084335, -111.4188657433597456 ) ) ;
#12012=VERTEX_POINT ( 'NONE', #1988 ) ;
#12026=DIRECTION ( 'NONE',  ( 0.000000000000000000, 0.000000000000000000, -1.000000000000000000 ) ) ;
#12035=ADVANCED_FACE ( 'NONE', ( #12636 ), #6097, .T. ) ;
#12052=DIRECTION ( 'NONE',  ( 0.000000000000000000, 0.000000000000000000, 1.000000000000000000 ) ) ;
#12060=CARTESIAN_POINT ( 'NONE',  ( 0.000000000000000000, 341.5974953295086038, -15.94751227074151956 ) ) ;
#12087=DIRECTION ( 'NONE',  ( -1.000000000000000000, -0.000000000000000000, -0.000000000000000000 ) ) ;
#12105=DIRECTION ( 'NONE',  ( -1.000000000000000000, 0.000000000000000000, 0.000000000000000000 ) ) ;
#12122=ORIENTED_EDGE ( 'NONE', *, *, #12641, .T. ) ;
#12134=DIRECTION ( 'NONE',  ( -1.000000000000000000, -0.000000000000000000, -0.000000000000000000 ) ) ;
#12159=CARTESIAN_POINT ( 'NONE',  ( 394.0000000000001137, 339.1725919290084335, -111.4188657433597456 ) ) ;
#12180=DIRECTION ( 'NONE',  ( 0.000000000000000000, -1.000000000000000000, 0.000000000000000000 ) ) ;
#12197=DIRECTION ( 'NONE',  ( 0.000000000000000000, 0.000000000000000000, 1.000000000000000000 ) ) ;
#12210=DIRECTION ( 'NONE',  ( -1.000000000000000000, -0.000000000000000000, -0.000000000000000000 ) ) ;
#12234=DIRECTION ( 'NONE',  ( 0.000000000000000000, 0.000000000000000000, -1.000000000000000000 ) ) ;
#12239=PLANE ( 'NONE',  #2338 ) ;
#12242=VERTEX_POINT ( 'NONE', #6695 ) ;
#12299=VERTEX_POINT ( 'NONE', #2931 ) ;
#12315=ORIENTED_EDGE ( 'NONE', *, *, #11938, .T. ) ;
#12371=DIRECTION ( 'NONE',  ( 1.000000000000000000, 0.000000000000000000, 0.000000000000000000 ) ) ;
#12373=ORIENTED_EDGE ( 'NONE', *, *, #15919, .T. ) ;
#12423=CARTESIAN_POINT ( 'NONE',  ( 394.0000000000001137, 240.7889724647196488, -104.9456657433598110 ) ) ;
#12433=CYLINDRICAL_SURFACE ( 'NONE', #15686, 0.7366000000000039183 ) ;
#12491=LINE ( 'NONE', #2173, #3942 ) ;
#12503=CARTESIAN_POINT ( 'NONE',  ( 394.0000000000001137, 339.3157724647196005, -16.41886574335978821 ) ) ;
#12512=VERTEX_POINT ( 'NONE', #1189 ) ;
#12528=ORIENTED_EDGE ( 'NONE', *, *, #2677, .T. ) ;
#12539=CARTESIAN_POINT ( 'NONE',  ( 394.0000000000001137, 240.7889724647196488, -10.68226574335980139 ) ) ;
#12582=DIRECTION ( 'NONE',  ( 0.000000000000000000, 0.000000000000000000, -1.000000000000000000 ) ) ;
#12583=VECTOR ( 'NONE', #13048, 1000.000000000000000 ) ;
#12588=CARTESIAN_POINT ( 'NONE',  ( 394.0000000000001137, 234.3157724647196289, -104.2090657433598011 ) ) ;
#12597=CARTESIAN_POINT ( 'NONE',  ( 0.000000000000000000, 240.7889724647196488, -17.15546574335979813 ) ) ;
#12619=SURFACE_STYLE_USAGE ( .BOTH. , #13920 ) ;
#12636=FACE_OUTER_BOUND ( 'NONE', #2496, .T. ) ;
#12638=CARTESIAN_POINT ( 'NONE',  ( 0.000000000000000000, 339.1725919290084335, -110.6822657433597925 ) ) ;
#12641=EDGE_CURVE ( 'NONE', #3874, #13380, #334, .T. ) ;
#12687=AXIS2_PLACEMENT_3D ( 'NONE', #11413, #13044, #16646 ) ;
#12720=PRODUCT_DEFINITION ( 'UNKNOWN', '', #5885, #11222 ) ;
#12728=VECTOR ( 'NONE', #11435, 1000.000000000000000 ) ;
#12782=LINE ( 'NONE', #11482, #14973 ) ;
#12807=ORIENTED_EDGE ( 'NONE', *, *, #10246, .T. ) ;
#12820=VERTEX_POINT ( 'NONE', #8486 ) ;
#12872=PRODUCT_DEFINITION_SHAPE ( 'NONE', 'NONE',  #12720 ) ;
#12885=DIRECTION ( 'NONE',  ( 0.000000000000000000, 0.000000000000000000, -1.000000000000000000 ) ) ;
#12897=CYLINDRICAL_SURFACE ( 'NONE', #2850, 0.7366000000000039183 ) ;
#12903=DIRECTION ( 'NONE',  ( 0.000000000000000000, 0.000000000000000000, 1.000000000000000000 ) ) ;
#12909=ORIENTED_EDGE ( 'NONE', *, *, #10358, .T. ) ;
#12924=VECTOR ( 'NONE', #4589, 1000.000000000000000 ) ;
#12962=SHAPE_REPRESENTATION ( 'Part8', ( #1488 ), #16580 ) ;
#12970=VECTOR ( 'NONE', #2396, 1000.000000000000000 ) ;
#12988=LINE ( 'NONE', #5233, #8069 ) ;
#12993=ORIENTED_EDGE ( 'NONE', *, *, #4546, .T. ) ;
#13020=VECTOR ( 'NONE', #9887, 1000.000000000000000 ) ;
#13044=DIRECTION ( 'NONE',  ( -1.000000000000000000, -0.000000000000000000, -0.000000000000000000 ) ) ;
#13048=DIRECTION ( 'NONE',  ( 0.000000000000000000, -1.000000000000000000, -1.321694076934710402E-16 ) ) ;
#13155=AXIS2_PLACEMENT_3D ( 'NONE', #6849, #5572, #10821 ) ;
#13170=EDGE_CURVE ( 'NONE', #16075, #1644, #5368, .T. ) ;
#13172=ORIENTED_EDGE ( 'NONE', *, *, #15398, .F. ) ;
#13178=FACE_OUTER_BOUND ( 'NONE', #9512, .T. ) ;
#13248=SHAPE_DEFINITION_REPRESENTATION ( #12872, #12962 ) ;
#13291=STYLED_ITEM ( 'NONE', ( #3273 ), #3164 ) ;
#13300=ADVANCED_FACE ( 'NONE', ( #5880 ), #16520, .T. ) ;
#13308=VECTOR ( 'NONE', #2029, 1000.000000000000000 ) ;
#13313=AXIS2_PLACEMENT_3D ( 'NONE', #88, #12105, #12197 ) ;
#13323=DIRECTION ( 'NONE',  ( -1.000000000000000000, -0.000000000000000000, -0.000000000000000000 ) ) ;
#13334=PLANE ( 'NONE',  #458 ) ;
#13350=LINE ( 'NONE', #4240, #6938 ) ;
#13374=LINE ( 'NONE', #6494, #12583 ) ;
#13380=VERTEX_POINT ( 'NONE', #2345 ) ;
#13386=CARTESIAN_POINT ( 'NONE',  ( 394.0000000000001137, 339.1725919290084335, -111.4188657433597456 ) ) ;
#13395=EDGE_CURVE ( 'NONE', #1365, #3462, #16684, .T. ) ;
#13407=PLANE ( 'NONE',  #13155 ) ;
#13412=CARTESIAN_POINT ( 'NONE',  ( 394.0000000000001137, 240.7889724647196488, -104.9456657433598110 ) ) ;
#13420=DIRECTION ( 'NONE',  ( -1.000000000000000000, -0.000000000000000000, -0.000000000000000000 ) ) ;
#13437=DIRECTION ( 'NONE',  ( 0.000000000000000000, 0.9271838545667903109, -0.3746065934159049093 ) ) ;
#13445=DIRECTION ( 'NONE',  ( 0.000000000000000000, 0.9271838545667884235, -0.3746065934159091837 ) ) ;
#13452=PLANE ( 'NONE',  #11822 ) ;
#13484=ORIENTED_EDGE ( 'NONE', *, *, #14351, .T. ) ;
#13513=EDGE_CURVE ( 'NONE', #11776, #5137, #14596, .T. ) ;
#13520=FACE_OUTER_BOUND ( 'NONE', #1288, .T. ) ;
#13525=CARTESIAN_POINT ( 'NONE',  ( 0.000000000000000000, 240.7889724647196488, -104.2090657433598011 ) ) ;
#13526=FACE_OUTER_BOUND ( 'NONE', #14810, .T. ) ;
#13539=AXIS2_PLACEMENT_3D ( 'NONE', #11533, #5004, #2689 ) ;
#13541=AXIS2_PLACEMENT_3D ( 'NONE', #6623, #11886, #129 ) ;
#13559=FACE_OUTER_BOUND ( 'NONE', #9653, .T. ) ;
#13576=APPLICATION_CONTEXT ( 'automotive_design' ) ;
#13587=DIRECTION ( 'NONE',  ( 0.000000000000000000, -1.000000000000000000, -1.321694076934710402E-16 ) ) ;
#13602=DIRECTION ( 'NONE',  ( -0.000000000000000000, 0.000000000000000000, -1.000000000000000000 ) ) ;
#13615=EDGE_LOOP ( 'NONE', ( #8131, #3889, #1801, #4398 ) ) ;
#13619=FACE_OUTER_BOUND ( 'NONE', #6480, .T. ) ;
#13628=AXIS2_PLACEMENT_3D ( 'NONE', #12597, #11308, #3501 ) ;
#13641=CARTESIAN_POINT ( 'NONE',  ( 0.000000000000000000, 341.5974953295075807, -105.4170192159777031 ) ) ;
#13661=EDGE_CURVE ( 'NONE', #3874, #2075, #4457, .T. ) ;
#13696=FACE_OUTER_BOUND ( 'NONE', #4880, .T. ) ;
#13699=ADVANCED_FACE ( 'NONE', ( #8159 ), #13407, .T. ) ;
#13738=ORIENTED_EDGE ( 'NONE', *, *, #15988, .T. ) ;
#13757=CARTESIAN_POINT ( 'NONE',  ( 394.0000000000001137, 339.1725919290087745, -10.68226574335978718 ) ) ;
#13791=ORIENTED_EDGE ( 'NONE', *, *, #11865, .T. ) ;
#13820=CIRCLE ( 'NONE', #3399, 0.7366000000000039183 ) ;
#13831=AXIS2_PLACEMENT_3D ( 'NONE', #9772, #7003, #7246 ) ;
#13857=EDGE_LOOP ( 'NONE', ( #11125, #250, #15815, #6791 ) ) ;
#13875=AXIS2_PLACEMENT_3D ( 'NONE', #14045, #11462, #16695 ) ;
#13882=EDGE_CURVE ( 'NONE', #14413, #7396, #11657, .T. ) ;
#13891=ORIENTED_EDGE ( 'NONE', *, *, #13970, .F. ) ;
#13912=LINE ( 'NONE', #15283, #15532 ) ;
#13920=SURFACE_SIDE_STYLE ('',( #3443 ) ) ;
#13924=CARTESIAN_POINT ( 'NONE',  ( 394.0000000000001137, 449.3157724647196005, -155.1251505852266632 ) ) ;
#13926=CIRCLE ( 'NONE', #6772, 6.473199999999998511 ) ;
#13932=LINE ( 'NONE', #6094, #5041 ) ;
#13969=EDGE_LOOP ( 'NONE', ( #2152, #2401, #284, #10137 ) ) ;
#13970=EDGE_CURVE ( 'NONE', #12012, #15132, #5642, .T. ) ;
#13990=DIRECTION ( 'NONE',  ( 0.000000000000000000, -0.3746065934159052424, 0.9271838545667901998 ) ) ;
#13991=ORIENTED_EDGE ( 'NONE', *, *, #16025, .T. ) ;
#13993=( GEOMETRIC_REPRESENTATION_CONTEXT ( 3 ) GLOBAL_UNCERTAINTY_ASSIGNED_CONTEXT ( ( #8240 ) ) GLOBAL_UNIT_ASSIGNED_CONTEXT ( ( #11087, #16574, #11499 ) ) REPRESENTATION_CONTEXT ( 'NONE', 'WORKASPACE' ) );
#14003=LINE ( 'NONE', #4633, #13020 ) ;
#14006=EDGE_CURVE ( 'NONE', #1082, #7330, #9338, .T. ) ;
#14013=DIRECTION ( 'NONE',  ( 0.000000000000000000, 0.000000000000000000, -1.000000000000000000 ) ) ;
#14032=DIRECTION ( 'NONE',  ( -1.000000000000000000, -0.000000000000000000, -0.000000000000000000 ) ) ;
#14037=VERTEX_POINT ( 'NONE', #831 ) ;
#14040=VECTOR ( 'NONE', #1448, 1000.000000000000000 ) ;
#14045=CARTESIAN_POINT ( 'NONE',  ( 394.0000000000001137, 339.3157724647196005, -104.9456657433597968 ) ) ;
#14101=LINE ( 'NONE', #2159, #10041 ) ;
#14103=COLOUR_RGB ( '', 0.08235294, 0.09019608, 0.10196078) ;
#14107=ORIENTED_EDGE ( 'NONE', *, *, #12641, .F. ) ;
#14118=FACE_OUTER_BOUND ( 'NONE', #2160, .T. ) ;
#14123=CARTESIAN_POINT ( 'NONE',  ( 394.0000000000001137, 341.5974953295075807, -105.4170192159777031 ) ) ;
#14159=VECTOR ( 'NONE', #13420, 1000.000000000000000 ) ;
#14181=ORIENTED_EDGE ( 'NONE', *, *, #770, .T. ) ;
#14194=CARTESIAN_POINT ( 'NONE',  ( 394.0000000000001137, 240.7889724647196488, -104.2090657433598011 ) ) ;
#14216=CARTESIAN_POINT ( 'NONE',  ( 0.000000000000000000, 240.7889724647196488, -110.6822657433598067 ) ) ;
#14225=CARTESIAN_POINT ( 'NONE',  ( 394.0000000000001137, 240.0523724647196389, -17.15546574335979813 ) ) ;
#14236=ORIENTED_EDGE ( 'NONE', *, *, #7526, .T. ) ;
#14273=ORIENTED_EDGE ( 'NONE', *, *, #15469, .F. ) ;
#14289=ORIENTED_EDGE ( 'NONE', *, *, #5840, .F. ) ;
#14295=ORIENTED_EDGE ( 'NONE', *, *, #15310, .T. ) ;
#14309=ADVANCED_FACE ( 'NONE', ( #13696 ), #8535, .T. ) ;
#14315=CARTESIAN_POINT ( 'NONE',  ( 394.0000000000001137, 339.4485271457189128, -10.62862937063367852 ) ) ;
#14320=DIRECTION ( 'NONE',  ( 0.000000000000000000, 0.000000000000000000, 1.000000000000000000 ) ) ;
#14351=EDGE_CURVE ( 'NONE', #7927, #583, #5872, .T. ) ;
#14370=AXIS2_PLACEMENT_3D ( 'NONE', #1992, #7223, #4730 ) ;
#14377=LINE ( 'NONE', #7656, #5847 ) ;
#14380=DIRECTION ( 'NONE',  ( 0.000000000000000000, -0.9271838545667884235, 0.3746065934159092392 ) ) ;
#14384=ORIENTED_EDGE ( 'NONE', *, *, #8048, .T. ) ;
#14413=VERTEX_POINT ( 'NONE', #14432 ) ;
#14432=CARTESIAN_POINT ( 'NONE',  ( 394.0000000000001137, 341.5974953295086038, -15.94751227074151956 ) ) ;
#14477=ORIENTED_EDGE ( 'NONE', *, *, #587, .T. ) ;
#14501=AXIS2_PLACEMENT_3D ( 'NONE', #8124, #14909, #8390 ) ;
#14510=ORIENTED_EDGE ( 'NONE', *, *, #10742, .F. ) ;
#14548=DIRECTION ( 'NONE',  ( 0.000000000000000000, 0.000000000000000000, 1.000000000000000000 ) ) ;
#14580=ORIENTED_EDGE ( 'NONE', *, *, #6625, .T. ) ;
#14596=LINE ( 'NONE', #6685, #6006 ) ;
#14607=DIRECTION ( 'NONE',  ( 0.000000000000000000, 1.000000000000000000, 1.321694076934710402E-16 ) ) ;
#14621=CYLINDRICAL_SURFACE ( 'NONE', #7432, 6.473200000000000287 ) ;
#14629=CIRCLE ( 'NONE', #13539, 6.473199999999998511 ) ;
#14664=CARTESIAN_POINT ( 'NONE',  ( 394.0000000000001137, 339.3157724647196005, -10.68226574335978718 ) ) ;
#14715=ORIENTED_EDGE ( 'NONE', *, *, #11927, .T. ) ;
#14728=ORIENTED_EDGE ( 'NONE', *, *, #696, .T. ) ;
#14735=ORIENTED_EDGE ( 'NONE', *, *, #4546, .F. ) ;
#14736=ORIENTED_EDGE ( 'NONE', *, *, #3971, .F. ) ;
#14741=AXIS2_PLACEMENT_3D ( 'NONE', #4242, #13437, #1660 ) ;
#14745=CARTESIAN_POINT ( 'NONE',  ( 394.0000000000001137, 339.1725919290084335, -110.6822657433597925 ) ) ;
#14776=FACE_OUTER_BOUND ( 'NONE', #3241, .T. ) ;
#14793=ORIENTED_EDGE ( 'NONE', *, *, #504, .F. ) ;
#14807=ORIENTED_EDGE ( 'NONE', *, *, #11303, .F. ) ;
#14810=EDGE_LOOP ( 'NONE', ( #7137, #14384, #16645, #13791 ) ) ;
#14814=ORIENTED_EDGE ( 'NONE', *, *, #3876, .T. ) ;
#14856=ADVANCED_FACE ( 'NONE', ( #7689 ), #10377, .T. ) ;
#14888=CARTESIAN_POINT ( 'NONE',  ( 394.0000000000001137, 234.3157724647196289, -104.2090657433598011 ) ) ;
#14897=ORIENTED_EDGE ( 'NONE', *, *, #16141, .T. ) ;
#14909=DIRECTION ( 'NONE',  ( -1.000000000000000000, -0.000000000000000000, -0.000000000000000000 ) ) ;
#14928=ADVANCED_FACE ( 'NONE', ( #9340 ), #6920, .T. ) ;
#14973=VECTOR ( 'NONE', #10294, 1000.000000000000114 ) ;
#14977=ADVANCED_FACE ( 'NONE', ( #13559 ), #8138, .T. ) ;
#15029=ORIENTED_EDGE ( 'NONE', *, *, #11938, .F. ) ;
#15033=ORIENTED_EDGE ( 'NONE', *, *, #15156, .F. ) ;
#15058=CARTESIAN_POINT ( 'NONE',  ( 394.0000000000001137, 240.7889724647196488, -104.9456657433598110 ) ) ;
#15074=DIRECTION ( 'NONE',  ( -1.000000000000000000, -0.000000000000000000, -0.000000000000000000 ) ) ;
#15089=ORIENTED_EDGE ( 'NONE', *, *, #504, .T. ) ;
#15106=EDGE_LOOP ( 'NONE', ( #9718, #5243, #12993, #14236 ) ) ;
#15132=VERTEX_POINT ( 'NONE', #834 ) ;
#15150=DIRECTION ( 'NONE',  ( -1.000000000000000000, 0.000000000000000000, 0.000000000000000000 ) ) ;
#15153=ORIENTED_EDGE ( 'NONE', *, *, #10742, .T. ) ;
#15156=EDGE_CURVE ( 'NONE', #1644, #11171, #1077, .T. ) ;
#15170=VECTOR ( 'NONE', #1066, 1000.000000000000000 ) ;
#15171=AXIS2_PLACEMENT_3D ( 'NONE', #1529, #12180, #16204 ) ;
#15217=DIRECTION ( 'NONE',  ( 1.000000000000000000, 0.000000000000000000, 0.000000000000000000 ) ) ;
#15222=LINE ( 'NONE', #13757, #5594 ) ;
#15254=FACE_OUTER_BOUND ( 'NONE', #16346, .T. ) ;
#15283=CARTESIAN_POINT ( 'NONE',  ( 0.000000000000000000, 341.5974953295086038, -15.94751227074151956 ) ) ;
#15288=CARTESIAN_POINT ( 'NONE',  ( 0.000000000000000000, 449.3157724647197142, 33.76061909850716347 ) ) ;
#15307=LINE ( 'NONE', #6183, #12728 ) ;
#15310=EDGE_CURVE ( 'NONE', #9087, #11776, #16016, .T. ) ;
#15315=ORIENTED_EDGE ( 'NONE', *, *, #10761, .T. ) ;
#15347=DIRECTION ( 'NONE',  ( 0.000000000000000000, 0.000000000000000000, 1.000000000000000000 ) ) ;
#15352=ORIENTED_EDGE ( 'NONE', *, *, #22, .T. ) ;
#15375=VECTOR ( 'NONE', #4919, 1000.000000000000000 ) ;
#15387=DIRECTION ( 'NONE',  ( 0.000000000000000000, 1.000000000000000000, 1.321694076934710402E-16 ) ) ;
#15394=ORIENTED_EDGE ( 'NONE', *, *, #4859, .F. ) ;
#15398=EDGE_CURVE ( 'NONE', #9815, #1644, #111, .T. ) ;
#15399=CARTESIAN_POINT ( 'NONE',  ( 0.000000000000000000, 339.1725919290084335, -104.9456657433597968 ) ) ;
#15424=AXIS2_PLACEMENT_3D ( 'NONE', #15058, #7143, #8281 ) ;
#15426=DIRECTION ( 'NONE',  ( 0.000000000000000000, 0.000000000000000000, 1.000000000000000000 ) ) ;
#15439=CARTESIAN_POINT ( 'NONE',  ( 394.0000000000001137, 341.5974953295086038, -15.94751227074151956 ) ) ;
#15462=VECTOR ( 'NONE', #16108, 1000.000000000000227 ) ;
#15469=EDGE_CURVE ( 'NONE', #1233, #12242, #12491, .T. ) ;
#15489=DIRECTION ( 'NONE',  ( 1.000000000000000000, 0.000000000000000000, -0.000000000000000000 ) ) ;
#15532=VECTOR ( 'NONE', #13990, 1000.000000000000000 ) ;
#15539=DIRECTION ( 'NONE',  ( 0.000000000000000000, 0.9271838545667883125, 0.3746065934159094613 ) ) ;
#15541=CARTESIAN_POINT ( 'NONE',  ( 394.0000000000001137, 234.3157724647196289, -104.2090657433598011 ) ) ;
#15565=LINE ( 'NONE', #5153, #1209 ) ;
#15617=LINE ( 'NONE', #2308, #5159 ) ;
#15619=ORIENTED_EDGE ( 'NONE', *, *, #10246, .F. ) ;
#15650=CARTESIAN_POINT ( 'NONE',  ( 394.0000000000001137, 339.1725919290087745, -16.41886574335978821 ) ) ;
#15677=ORIENTED_EDGE ( 'NONE', *, *, #2895, .F. ) ;
#15686=AXIS2_PLACEMENT_3D ( 'NONE', #16385, #678, #7098 ) ;
#15687=VECTOR ( 'NONE', #7233, 1000.000000000000000 ) ;
#15702=LINE ( 'NONE', #3950, #12970 ) ;
#15718=CARTESIAN_POINT ( 'NONE',  ( 0.000000000000000000, 339.4485271457189128, -10.62862937063367852 ) ) ;
#15723=ORIENTED_EDGE ( 'NONE', *, *, #15874, .F. ) ;
#15733=LINE ( 'NONE', #3887, #8284 ) ;
#15813=PLANE ( 'NONE',  #6130 ) ;
#15815=ORIENTED_EDGE ( 'NONE', *, *, #4265, .F. ) ;
#15844=DIRECTION ( 'NONE',  ( 0.000000000000000000, 0.000000000000000000, -1.000000000000000000 ) ) ;
#15848=DIRECTION ( 'NONE',  ( 0.000000000000000000, 0.000000000000000000, 1.000000000000000000 ) ) ;
#15874=EDGE_CURVE ( 'NONE', #7289, #15132, #15222, .T. ) ;
#15878=DIRECTION ( 'NONE',  ( 0.000000000000000000, -0.9271838545667883125, -0.3746065934159096278 ) ) ;
#15883=CARTESIAN_POINT ( 'NONE',  ( 394.0000000000001137, 339.3157724647196005, -110.6822657433597925 ) ) ;
#15911=DIRECTION ( 'NONE',  ( 0.000000000000000000, -0.3746065934159092392, -0.9271838545667885345 ) ) ;
#15919=EDGE_CURVE ( 'NONE', #15132, #1879, #7770, .T. ) ;
#15946=VECTOR ( 'NONE', #3682, 1000.000000000000000 ) ;
#15988=EDGE_CURVE ( 'NONE', #1572, #14413, #16492, .T. ) ;
#16016=LINE ( 'NONE', #2786, #16292 ) ;
#16025=EDGE_CURVE ( 'NONE', #4334, #5519, #13932, .T. ) ;
#16075=VERTEX_POINT ( 'NONE', #11593 ) ;
#16097=DIRECTION ( 'NONE',  ( 0.000000000000000000, 0.000000000000000000, -1.000000000000000000 ) ) ;
#16108=DIRECTION ( 'NONE',  ( 0.000000000000000000, -0.9271838545667884235, 0.3746065934159092392 ) ) ;
#16141=EDGE_CURVE ( 'NONE', #8784, #12820, #3788, .T. ) ;
#16160=EDGE_LOOP ( 'NONE', ( #15394, #5807, #14477, #2962 ) ) ;
#16195=LINE ( 'NONE', #4434, #8621 ) ;
#16204=DIRECTION ( 'NONE',  ( 0.000000000000000000, -0.000000000000000000, -1.000000000000000000 ) ) ;
#16262=AXIS2_PLACEMENT_3D ( 'NONE', #4598, #15074, #12582 ) ;
#16281=ORIENTED_EDGE ( 'NONE', *, *, #7029, .T. ) ;
#16292=VECTOR ( 'NONE', #6732, 1000.000000000000000 ) ;
#16301=ORIENTED_EDGE ( 'NONE', *, *, #10442, .T. ) ;
#16337=EDGE_CURVE ( 'NONE', #1233, #6598, #8242, .T. ) ;
#16346=EDGE_LOOP ( 'NONE', ( #4152, #16428, #15033, #12909 ) ) ;
#16377=PLANE ( 'NONE',  #8804 ) ;
#16385=CARTESIAN_POINT ( 'NONE',  ( 394.0000000000001137, 339.1725919290084335, -111.4188657433597456 ) ) ;
#16402=DIRECTION ( 'NONE',  ( -1.000000000000000000, -0.000000000000000000, -0.000000000000000000 ) ) ;
#16428=ORIENTED_EDGE ( 'NONE', *, *, #9636, .F. ) ;
#16477=CARTESIAN_POINT ( 'NONE',  ( 0.000000000000000000, 339.1725919290087745, -9.945665743359786148 ) ) ;
#16480=EDGE_CURVE ( 'NONE', #7289, #1572, #11106, .T. ) ;
#16492=LINE ( 'NONE', #3369, #8903 ) ;
#16506=ADVANCED_FACE ( 'NONE', ( #6472 ), #11729, .T. ) ;
#16520=PLANE ( 'NONE',  #3278 ) ;
#16537=EDGE_CURVE ( 'NONE', #49, #9826, #16875, .T. ) ;
#16539=EDGE_CURVE ( 'NONE', #9815, #9087, #16953, .T. ) ;
#16571=ORIENTED_EDGE ( 'NONE', *, *, #1960, .T. ) ;
#16574=( NAMED_UNIT ( * ) PLANE_ANGLE_UNIT ( ) SI_UNIT ( $, .RADIAN. ) );
#16580=( GEOMETRIC_REPRESENTATION_CONTEXT ( 3 ) GLOBAL_UNCERTAINTY_ASSIGNED_CONTEXT ( ( #5668 ) ) GLOBAL_UNIT_ASSIGNED_CONTEXT ( ( #4828, #4909, #7229 ) ) REPRESENTATION_CONTEXT ( 'NONE', 'WORKASPACE' ) );
#16616=PLANE ( 'NONE',  #10414 ) ;
#16645=ORIENTED_EDGE ( 'NONE', *, *, #890, .F. ) ;
#16646=DIRECTION ( 'NONE',  ( 0.000000000000000000, 0.000000000000000000, 1.000000000000000000 ) ) ;
#16665=CARTESIAN_POINT ( 'NONE',  ( 0.000000000000000000, 240.7889724647196488, -104.2090657433598011 ) ) ;
#16672=VERTEX_POINT ( 'NONE', #1597 ) ;
#16684=LINE ( 'NONE', #8722, #15375 ) ;
#16695=DIRECTION ( 'NONE',  ( 0.000000000000000000, 1.000000000000000000, 1.321694076934710402E-16 ) ) ;
#16699=DIRECTION ( 'NONE',  ( -0.000000000000000000, 0.000000000000000000, -1.000000000000000000 ) ) ;
#16704=EDGE_CURVE ( 'NONE', #5519, #11776, #5366, .T. ) ;
#16731=PLANE ( 'NONE',  #9701 ) ;
#16758=ORIENTED_EDGE ( 'NONE', *, *, #13395, .F. ) ;
#16775=CARTESIAN_POINT ( 'NONE',  ( 394.0000000000001137, 339.4485271457185718, -110.7359021160857537 ) ) ;
#16781=CIRCLE ( 'NONE', #8002, 6.473199999999998511 ) ;
#16797=AXIS2_PLACEMENT_3D ( 'NONE', #12060, #3041, #14548 ) ;
#16875=LINE ( 'NONE', #1337, #11895 ) ;
#16887=VECTOR ( 'NONE', #7693, 999.9999999999998863 ) ;
#16896=LINE ( 'NONE', #15541, #14040 ) ;
#16897=CIRCLE ( 'NONE', #13628, 6.473199999999998511 ) ;
#16939=FACE_OUTER_BOUND ( 'NONE', #3649, .T. ) ;
#16941=CARTESIAN_POINT ( 'NONE',  ( 394.0000000000001137, 451.4647406485092915, -149.8062676851188257 ) ) ;
#16953=LINE ( 'NONE', #10525, #8881 ) ;
ENDSEC;
END-ISO-10303-21;
